ISO-10303-21;
HEADER;
FILE_DESCRIPTION (('STEP AP214'),
    '1' );
FILE_NAME ('722909.step',
    '2026-11-01T05:08:46',
    ( '' ),
    ( '' ),
    'SwSTEP 2.0',
    'SolidWorks 2024',
    '' );
FILE_SCHEMA (( 'AUTOMOTIVE_DESIGN' ));
ENDSEC;

DATA;
#30=DIRECTION ( 'NONE',  ( 0.000000000000000000, 1.000000000000000000, 0.000000000000000000 ) ) ;
#33=DIRECTION ( 'NONE',  ( -1.000000000000000000, 0.000000000000000000, 0.000000000000000000 ) ) ;
#46=DIRECTION ( 'NONE',  ( 1.000000000000000000, 0.000000000000000000, 0.000000000000000000 ) ) ;
#77=AXIS2_PLACEMENT_3D ( 'NONE', #8422, #7109, #16564 ) ;
#81=DIRECTION ( 'NONE',  ( -1.000000000000000000, 0.000000000000000000, 0.000000000000000000 ) ) ;
#92=CIRCLE ( 'NONE', #3112, 15.14120580695350071 ) ;
#117=VERTEX_POINT ( 'NONE', #2818 ) ;
#141=DIRECTION ( 'NONE',  ( 0.000000000000000000, 1.000000000000000000, 0.000000000000000000 ) ) ;
#155=VERTEX_POINT ( 'NONE', #13316 ) ;
#166=DIRECTION ( 'NONE',  ( 1.000000000000000000, 0.000000000000000000, 0.000000000000000000 ) ) ;
#186=DIRECTION ( 'NONE',  ( 1.000000000000000000, 0.000000000000000000, 0.000000000000000000 ) ) ;
#188=CARTESIAN_POINT ( 'NONE',  ( 5.425003271131650706, 0.000000000000000000, 0.000000000000000000 ) ) ;
#199=VERTEX_POINT ( 'NONE', #9610 ) ;
#210=CARTESIAN_POINT ( 'NONE',  ( 1.050000000000000044, 16.38749999999999929, 0.000000000000000000 ) ) ;
#212=( GEOMETRIC_REPRESENTATION_CONTEXT ( 3 ) GLOBAL_UNCERTAINTY_ASSIGNED_CONTEXT ( ( #10025 ) ) GLOBAL_UNIT_ASSIGNED_CONTEXT ( ( #1452, #15788, #15621 ) ) REPRESENTATION_CONTEXT ( 'NONE', 'WORKASPACE' ) );
#234=DIRECTION ( 'NONE',  ( -0.7327934916262990317, 0.6804510993672779895, 0.000000000000000000 ) ) ;
#291=DIRECTION ( 'NONE',  ( 0.000000000000000000, 1.000000000000000000, 0.000000000000000000 ) ) ;
#309=ADVANCED_FACE ( 'NONE', ( #6149 ), #10481, .F. ) ;
#323=ORIENTED_EDGE ( 'NONE', *, *, #3232, .T. ) ;
#335=DIRECTION ( 'NONE',  ( 1.000000000000000000, 0.000000000000000000, 0.000000000000000000 ) ) ;
#342=DIRECTION ( 'NONE',  ( 0.000000000000000000, 1.000000000000000000, 0.000000000000000000 ) ) ;
#353=FACE_BOUND ( 'NONE', #6381, .T. ) ;
#376=CARTESIAN_POINT ( 'NONE',  ( 1.574999999999999956, 0.000000000000000000, 0.000000000000000000 ) ) ;
#381=VECTOR ( 'NONE', #9762, 1000.000000000000227 ) ;
#384=LINE ( 'NONE', #9232, #10078 ) ;
#404=EDGE_CURVE ( 'NONE', #14628, #16915, #11476, .T. ) ;
#424=DIRECTION ( 'NONE',  ( 0.000000000000000000, 1.000000000000000000, 0.000000000000000000 ) ) ;
#425=AXIS2_PLACEMENT_3D ( 'NONE', #9617, #14854, #342 ) ;
#434=PRODUCT_DEFINITION_CONTEXT ( 'detailed design', #8850, 'design' ) ;
#503=ADVANCED_FACE ( 'NONE', ( #14570 ), #12397, .T. ) ;
#516=DIRECTION ( 'NONE',  ( 1.000000000000000000, 0.000000000000000000, 0.000000000000000000 ) ) ;
#517=CARTESIAN_POINT ( 'NONE',  ( -1.776356839400249676E-15, 0.000000000000000000, 0.000000000000000000 ) ) ;
#551=FACE_OUTER_BOUND ( 'NONE', #9723, .T. ) ;
#585=FACE_OUTER_BOUND ( 'NONE', #12046, .T. ) ;
#586=EDGE_LOOP ( 'NONE', ( #4983, #9221, #13584, #12457 ) ) ;
#589=EDGE_CURVE ( 'NONE', #6207, #14628, #14828, .T. ) ;
#692=CARTESIAN_POINT ( 'NONE',  ( 4.899999999999999467, -12.00000000000000000, 1.509263698769704680E-15 ) ) ;
#702=DIRECTION ( 'NONE',  ( 0.000000000000000000, 1.000000000000000000, 0.000000000000000000 ) ) ;
#756=DIRECTION ( 'NONE',  ( 0.000000000000000000, 0.000000000000000000, -1.000000000000000000 ) ) ;
#793=VERTEX_POINT ( 'NONE', #4923 ) ;
#805=ORIENTED_EDGE ( 'NONE', *, *, #924, .T. ) ;
#810=EDGE_LOOP ( 'NONE', ( #14772, #2703, #1157, #4328 ) ) ;
#843=DIRECTION ( 'NONE',  ( 0.000000000000000000, 1.000000000000000000, 0.000000000000000000 ) ) ;
#849=AXIS2_PLACEMENT_3D ( 'NONE', #14924, #3166, #8401 ) ;
#865=ORIENTED_EDGE ( 'NONE', *, *, #2062, .F. ) ;
#924=EDGE_CURVE ( 'NONE', #11643, #9884, #15834, .T. ) ;
#968=CYLINDRICAL_SURFACE ( 'NONE', #6957, 14.59999999999999964 ) ;
#986=DIRECTION ( 'NONE',  ( 1.000000000000000000, 0.000000000000000000, 0.000000000000000000 ) ) ;
#991=AXIS2_PLACEMENT_3D ( 'NONE', #12113, #186, #5407 ) ;
#1026=DIRECTION ( 'NONE',  ( -1.000000000000000000, 0.000000000000000000, 0.000000000000000000 ) ) ;
#1031=LINE ( 'NONE', #2469, #4368 ) ;
#1047=ORIENTED_EDGE ( 'NONE', *, *, #5725, .F. ) ;
#1079=ADVANCED_FACE ( 'NONE', ( #551 ), #6362, .T. ) ;
#1087=EDGE_CURVE ( 'NONE', #155, #13073, #8039, .T. ) ;
#1098=LINE ( 'NONE', #6161, #11861 ) ;
#1142=VERTEX_POINT ( 'NONE', #4034 ) ;
#1144=CARTESIAN_POINT ( 'NONE',  ( 1.050000000000000044, -17.52499999999999858, -2.146193515505736390E-15 ) ) ;
#1146=DIRECTION ( 'NONE',  ( 0.000000000000000000, 1.000000000000000000, 0.000000000000000000 ) ) ;
#1157=ORIENTED_EDGE ( 'NONE', *, *, #12746, .F. ) ;
#1159=DIRECTION ( 'NONE',  ( 0.000000000000000000, 1.000000000000000000, 0.000000000000000000 ) ) ;
#1217=EDGE_LOOP ( 'NONE', ( #865, #11206, #10156, #13235 ) ) ;
#1284=ADVANCED_FACE ( 'NONE', ( #14336 ), #15957, .T. ) ;
#1298=FACE_OUTER_BOUND ( 'NONE', #8169, .T. ) ;
#1309=VECTOR ( 'NONE', #7352, 1000.000000000000000 ) ;
#1315=DIRECTION ( 'NONE',  ( 1.000000000000000000, 0.000000000000000000, 0.000000000000000000 ) ) ;
#1333=FACE_OUTER_BOUND ( 'NONE', #14794, .T. ) ;
#1348=CIRCLE ( 'NONE', #9342, 17.85000000000000142 ) ;
#1398=DIRECTION ( 'NONE',  ( 0.000000000000000000, 1.000000000000000000, 0.000000000000000000 ) ) ;
#1427=DIRECTION ( 'NONE',  ( 1.000000000000000000, 0.000000000000000000, 0.000000000000000000 ) ) ;
#1452=( LENGTH_UNIT ( ) NAMED_UNIT ( * ) SI_UNIT ( .MILLI., .METRE. ) );
#1471=CIRCLE ( 'NONE', #6667, 12.64814671169700055 ) ;
#1488=AXIS2_PLACEMENT_3D ( 'NONE', #3280, #8693, #15217 ) ;
#1492=PLANE ( 'NONE',  #8426 ) ;
#1523=EDGE_CURVE ( 'NONE', #16479, #11116, #10748, .T. ) ;
#1539=DIRECTION ( 'NONE',  ( 0.000000000000000000, 1.000000000000000000, 0.000000000000000000 ) ) ;
#1551=ORIENTED_EDGE ( 'NONE', *, *, #4342, .T. ) ;
#1554=VECTOR ( 'NONE', #4294, 1000.000000000000227 ) ;
#1557=AXIS2_PLACEMENT_3D ( 'NONE', #2859, #4333, #8184 ) ;
#1587=ORIENTED_EDGE ( 'NONE', *, *, #12196, .F. ) ;
#1590=EDGE_LOOP ( 'NONE', ( #4710, #5553, #13840, #8321, #11637 ) ) ;
#1614=EDGE_CURVE ( 'NONE', #793, #11643, #14822, .T. ) ;
#1643=ORIENTED_EDGE ( 'NONE', *, *, #7318, .F. ) ;
#1657=CONICAL_SURFACE ( 'NONE', #11250, 13.62500000000000000, 0.2281026282799422378 ) ;
#1677=FACE_OUTER_BOUND ( 'NONE', #1217, .T. ) ;
#1679=CARTESIAN_POINT ( 'NONE',  ( 2.799999999999999822, 0.000000000000000000, 0.000000000000000000 ) ) ;
#1704=DIRECTION ( 'NONE',  ( 1.000000000000000000, 0.000000000000000000, 0.000000000000000000 ) ) ;
#1716=UNCERTAINTY_MEASURE_WITH_UNIT (LENGTH_MEASURE( 1.000000000000000082E-05 ), #13062, 'distance_accuracy_value', 'NONE');
#1720=PLANE ( 'NONE',  #7764 ) ;
#1742=ORIENTED_EDGE ( 'NONE', *, *, #4581, .T. ) ;
#1770=AXIS2_PLACEMENT_3D ( 'NONE', #6530, #11967, #291 ) ;
#1773=DIRECTION ( 'NONE',  ( 0.9999937692730440641, -0.003530072958125829961, 4.323092548925426475E-19 ) ) ;
#1890=FACE_OUTER_BOUND ( 'NONE', #15812, .T. ) ;
#1921=DIRECTION ( 'NONE',  ( 1.000000000000000000, 0.000000000000000000, 0.000000000000000000 ) ) ;
#1929=DIRECTION ( 'NONE',  ( 0.000000000000000000, 1.000000000000000000, 0.000000000000000000 ) ) ;
#1939=EDGE_CURVE ( 'NONE', #6725, #11290, #5326, .T. ) ;
#1940=ADVANCED_FACE ( 'NONE', ( #1890 ), #10999, .T. ) ;
#2005=EDGE_CURVE ( 'NONE', #12856, #6207, #14791, .T. ) ;
#2018=ORIENTED_EDGE ( 'NONE', *, *, #13805, .F. ) ;
#2026=DIRECTION ( 'NONE',  ( 0.000000000000000000, 1.000000000000000000, 0.000000000000000000 ) ) ;
#2034=VECTOR ( 'NONE', #2855, 1000.000000000000000 ) ;
#2043=LINE ( 'NONE', #14338, #8366 ) ;
#2057=DIRECTION ( 'NONE',  ( 0.000000000000000000, 1.000000000000000000, 0.000000000000000000 ) ) ;
#2062=EDGE_CURVE ( 'NONE', #117, #2600, #1031, .T. ) ;
#2064=CARTESIAN_POINT ( 'NONE',  ( 5.162501635565829972, 0.000000000000000000, 0.000000000000000000 ) ) ;
#2101=CYLINDRICAL_SURFACE ( 'NONE', #14180, 18.50000000000000000 ) ;
#2108=CONICAL_SURFACE ( 'NONE', #9492, 14.92500000000000071, 1.076854957875310381 ) ;
#2220=AXIS2_PLACEMENT_3D ( 'NONE', #6030, #13775, #6194 ) ;
#2257=CARTESIAN_POINT ( 'NONE',  ( 1.750000000000000000, 14.59999999999999964, 0.000000000000000000 ) ) ;
#2302=CARTESIAN_POINT ( 'NONE',  ( 3.674999999999999822, 0.000000000000000000, 0.000000000000000000 ) ) ;
#2306=FACE_OUTER_BOUND ( 'NONE', #12787, .T. ) ;
#2351=AXIS2_PLACEMENT_3D ( 'NONE', #9806, #8505, #13745 ) ;
#2379=CIRCLE ( 'NONE', #1557, 14.59999999999999964 ) ;
#2382=CARTESIAN_POINT ( 'NONE',  ( 5.687501635565830327, 12.64907335584850046, 0.000000000000000000 ) ) ;
#2423=CARTESIAN_POINT ( 'NONE',  ( 5.950000000000000178, -12.65000000000000036, -1.701720561796546765E-15 ) ) ;
#2427=DIRECTION ( 'NONE',  ( -1.000000000000000000, 0.000000000000000000, 0.000000000000000000 ) ) ;
#2467=ORIENTED_EDGE ( 'NONE', *, *, #2534, .F. ) ;
#2469=CARTESIAN_POINT ( 'NONE',  ( 4.025000000000000355, -17.52499999999999858, -2.146193515505736390E-15 ) ) ;
#2472=CARTESIAN_POINT ( 'NONE',  ( 1.750000000000000000, 0.000000000000000000, 0.000000000000000000 ) ) ;
#2477=EDGE_CURVE ( 'NONE', #12375, #16649, #92, .T. ) ;
#2515=AXIS2_PLACEMENT_3D ( 'NONE', #2624, #15594, #7852 ) ;
#2529=LINE ( 'NONE', #9155, #8040 ) ;
#2533=CARTESIAN_POINT ( 'NONE',  ( 4.899999999999999467, 12.00000000000000000, 0.000000000000000000 ) ) ;
#2534=EDGE_CURVE ( 'NONE', #6207, #5894, #2830, .T. ) ;
#2556=CIRCLE ( 'NONE', #8051, 17.52499999999999858 ) ;
#2557=CARTESIAN_POINT ( 'NONE',  ( -1.776356839400249676E-15, 13.94999999999999929, 0.000000000000000000 ) ) ;
#2563=VERTEX_POINT ( 'NONE', #3810 ) ;
#2568=AXIS2_PLACEMENT_3D ( 'NONE', #16342, #16495, #7219 ) ;
#2574=EDGE_CURVE ( 'NONE', #11116, #793, #10418, .T. ) ;
#2598=ORIENTED_EDGE ( 'NONE', *, *, #8043, .T. ) ;
#2600=VERTEX_POINT ( 'NONE', #1144 ) ;
#2601=LINE ( 'NONE', #3727, #14590 ) ;
#2624=CARTESIAN_POINT ( 'NONE',  ( 4.899999999999999467, 0.000000000000000000, 0.000000000000000000 ) ) ;
#2639=DIRECTION ( 'NONE',  ( 1.000000000000000000, 0.000000000000000000, 0.000000000000000000 ) ) ;
#2654=ADVANCED_FACE ( 'NONE', ( #6537 ), #6929, .T. ) ;
#2703=ORIENTED_EDGE ( 'NONE', *, *, #2062, .T. ) ;
#2712=CARTESIAN_POINT ( 'NONE',  ( 3.674999999999999822, 14.43750000000000000, 0.000000000000000000 ) ) ;
#2731=CARTESIAN_POINT ( 'NONE',  ( 2.799999999999999822, -13.30000000000000071, -1.628780242865979955E-15 ) ) ;
#2750=DIRECTION ( 'NONE',  ( 0.000000000000000000, 1.000000000000000000, 0.000000000000000000 ) ) ;
#2807=VECTOR ( 'NONE', #8114, 1000.000000000000000 ) ;
#2814=VERTEX_POINT ( 'NONE', #13942 ) ;
#2815=DIRECTION ( 'NONE',  ( 0.000000000000000000, 1.000000000000000000, -1.224646799147353207E-16 ) ) ;
#2818=CARTESIAN_POINT ( 'NONE',  ( 7.000000000000000000, -17.52499999999999858, -2.146193515505736390E-15 ) ) ;
#2830=CIRCLE ( 'NONE', #5015, 14.27500000000000036 ) ;
#2855=DIRECTION ( 'NONE',  ( 0.7327934916262990317, 0.6804510993672779895, 0.000000000000000000 ) ) ;
#2859=CARTESIAN_POINT ( 'NONE',  ( 3.500000000000000000, 0.000000000000000000, 0.000000000000000000 ) ) ;
#2869=VERTEX_POINT ( 'NONE', #3546 ) ;
#2875=CARTESIAN_POINT ( 'NONE',  ( 6.649999999999999467, -18.17500000000000071, -2.225795557450314789E-15 ) ) ;
#2897=ADVANCED_FACE ( 'NONE', ( #1298 ), #968, .T. ) ;
#2918=AXIS2_PLACEMENT_3D ( 'NONE', #5044, #3598, #15614 ) ;
#2939=LINE ( 'NONE', #9555, #3421 ) ;
#2975=VECTOR ( 'NONE', #1773, 1000.000000000000227 ) ;
#2982=CYLINDRICAL_SURFACE ( 'NONE', #12438, 15.25000000000000000 ) ;
#2985=AXIS2_PLACEMENT_3D ( 'NONE', #4628, #11083, #2057 ) ;
#2992=LINE ( 'NONE', #4450, #1554 ) ;
#3003=AXIS2_PLACEMENT_3D ( 'NONE', #517, #14778, #8233 ) ;
#3034=CONICAL_SURFACE ( 'NONE', #9057, 18.17500000000000071, 0.7483780475235185525 ) ;
#3063=ORIENTED_EDGE ( 'NONE', *, *, #11915, .F. ) ;
#3108=CARTESIAN_POINT ( 'NONE',  ( 5.950000000000000178, 0.000000000000000000, 0.000000000000000000 ) ) ;
#3112=AXIS2_PLACEMENT_3D ( 'NONE', #6363, #11624, #7742 ) ;
#3114=CIRCLE ( 'NONE', #5287, 12.65000000000000036 ) ;
#3166=DIRECTION ( 'NONE',  ( 1.000000000000000000, 0.000000000000000000, 0.000000000000000000 ) ) ;
#3172=CARTESIAN_POINT ( 'NONE',  ( 3.850000000000000089, 0.000000000000000000, -14.27500000000000036 ) ) ;
#3180=CARTESIAN_POINT ( 'NONE',  ( 3.674999999999999822, -14.43750000000000000, -1.768083816268991068E-15 ) ) ;
#3232=EDGE_CURVE ( 'NONE', #16915, #11290, #3575, .T. ) ;
#3253=CARTESIAN_POINT ( 'NONE',  ( 6.299999999999999822, 0.000000000000000000, 0.000000000000000000 ) ) ;
#3257=ORIENTED_EDGE ( 'NONE', *, *, #4665, .F. ) ;
#3269=DIRECTION ( 'NONE',  ( 1.000000000000000000, 0.000000000000000000, 0.000000000000000000 ) ) ;
#3271=EDGE_CURVE ( 'NONE', #8018, #7469, #8547, .T. ) ;
#3280=CARTESIAN_POINT ( 'NONE',  ( 0.000000000000000000, 0.000000000000000000, 0.000000000000000000 ) ) ;
#3290=AXIS2_PLACEMENT_3D ( 'NONE', #3340, #8750, #13821 ) ;
#3323=CARTESIAN_POINT ( 'NONE',  ( 5.950000000000000178, 0.000000000000000000, 0.000000000000000000 ) ) ;
#3330=CARTESIAN_POINT ( 'NONE',  ( 5.425003271131650706, 12.64814671169700055, 0.000000000000000000 ) ) ;
#3332=DIRECTION ( 'NONE',  ( 0.000000000000000000, 1.000000000000000000, 0.000000000000000000 ) ) ;
#3340=CARTESIAN_POINT ( 'NONE',  ( 1.399999999999999911, 0.000000000000000000, 0.000000000000000000 ) ) ;
#3377=VERTEX_POINT ( 'NONE', #2731 ) ;
#3379=AXIS2_PLACEMENT_3D ( 'NONE', #9779, #7257, #756 ) ;
#3384=ORIENTED_EDGE ( 'NONE', *, *, #1614, .F. ) ;
#3391=CIRCLE ( 'NONE', #6390, 15.14120580695350071 ) ;
#3421=VECTOR ( 'NONE', #13340, 1000.000000000000114 ) ;
#3543=EDGE_CURVE ( 'NONE', #199, #8018, #10196, .T. ) ;
#3546=CARTESIAN_POINT ( 'NONE',  ( 3.850000000000000089, -14.27500000000000036, -1.768083816268991068E-15 ) ) ;
#3548=ORIENTED_EDGE ( 'NONE', *, *, #10274, .F. ) ;
#3575=CIRCLE ( 'NONE', #4932, 14.59999999999999964 ) ;
#3598=DIRECTION ( 'NONE',  ( -1.000000000000000000, 0.000000000000000000, 0.000000000000000000 ) ) ;
#3655=EDGE_LOOP ( 'NONE', ( #3384, #15512, #6964, #8620 ) ) ;
#3727=CARTESIAN_POINT ( 'NONE',  ( 4.025000000000000355, 17.52499999999999858, 0.000000000000000000 ) ) ;
#3746=CARTESIAN_POINT ( 'NONE',  ( 5.569974746830579804, 0.000000000000000000, 0.000000000000000000 ) ) ;
#3751=DIRECTION ( 'NONE',  ( -0.8502651466878615727, 0.5263546146162958461, 0.000000000000000000 ) ) ;
#3781=CARTESIAN_POINT ( 'NONE',  ( 4.549999999999999822, 0.000000000000000000, 0.000000000000000000 ) ) ;
#3810=CARTESIAN_POINT ( 'NONE',  ( 6.299999999999999822, 18.50000000000000000, 0.000000000000000000 ) ) ;
#3853=DIRECTION ( 'NONE',  ( 0.000000000000000000, 1.000000000000000000, 0.000000000000000000 ) ) ;
#3855=DIRECTION ( 'NONE',  ( 0.000000000000000000, 1.000000000000000000, 0.000000000000000000 ) ) ;
#3873=FACE_OUTER_BOUND ( 'NONE', #4063, .T. ) ;
#3878=ORIENTED_EDGE ( 'NONE', *, *, #13612, .F. ) ;
#3882=VECTOR ( 'NONE', #8384, 1000.000000000000114 ) ;
#3884=EDGE_LOOP ( 'NONE', ( #7231, #1643, #11519, #4340 ) ) ;
#3898=ORIENTED_EDGE ( 'NONE', *, *, #15895, .F. ) ;
#3924=CARTESIAN_POINT ( 'NONE',  ( 2.625000000000000000, 0.000000000000000000, 0.000000000000000000 ) ) ;
#3984=PRODUCT_DEFINITION_FORMATION_WITH_SPECIFIED_SOURCE ( 'ANY', '', #8762, .NOT_KNOWN. ) ;
#3991=CARTESIAN_POINT ( 'NONE',  ( 6.649999999999999467, 0.000000000000000000, 0.000000000000000000 ) ) ;
#4014=CYLINDRICAL_SURFACE ( 'NONE', #5704, 14.59999999999999964 ) ;
#4034=CARTESIAN_POINT ( 'NONE',  ( -8.881784197001250351E-16, -17.85000000000000142, 2.225795557450314789E-15 ) ) ;
#4059=ORIENTED_EDGE ( 'NONE', *, *, #2574, .F. ) ;
#4063=EDGE_LOOP ( 'NONE', ( #12236, #5924, #16175, #9261 ) ) ;
#4087=ORIENTED_EDGE ( 'NONE', *, *, #12760, .T. ) ;
#4092=CARTESIAN_POINT ( 'NONE',  ( 4.549999999999999822, 0.000000000000000000, 0.000000000000000000 ) ) ;
#4111=ORIENTED_EDGE ( 'NONE', *, *, #2574, .T. ) ;
#4121=EDGE_CURVE ( 'NONE', #3377, #9012, #2939, .T. ) ;
#4132=EDGE_CURVE ( 'NONE', #11643, #13527, #6150, .T. ) ;
#4208=CARTESIAN_POINT ( 'NONE',  ( 5.950000000000000178, 12.65000000000000036, 0.000000000000000000 ) ) ;
#4229=ORIENTED_EDGE ( 'NONE', *, *, #16927, .T. ) ;
#4244=AXIS2_PLACEMENT_3D ( 'NONE', #3108, #16157, #5680 ) ;
#4294=DIRECTION ( 'NONE',  ( -0.003530072958128175308, 0.9999937692730440641, 0.000000000000000000 ) ) ;
#4322=ADVANCED_FACE ( 'NONE', ( #8510 ), #15218, .T. ) ;
#4328=ORIENTED_EDGE ( 'NONE', *, *, #10365, .F. ) ;
#4333=DIRECTION ( 'NONE',  ( 1.000000000000000000, 0.000000000000000000, 0.000000000000000000 ) ) ;
#4340=ORIENTED_EDGE ( 'NONE', *, *, #10274, .T. ) ;
#4342=EDGE_CURVE ( 'NONE', #14244, #16161, #2043, .T. ) ;
#4366=DIRECTION ( 'NONE',  ( 0.000000000000000000, 1.000000000000000000, 0.000000000000000000 ) ) ;
#4368=VECTOR ( 'NONE', #11493, 1000.000000000000000 ) ;
#4401=CIRCLE ( 'NONE', #4930, 0.6999999999999992895 ) ;
#4410=ORIENTED_EDGE ( 'NONE', *, *, #4121, .F. ) ;
#4450=CARTESIAN_POINT ( 'NONE',  ( 5.945602903476760126, 13.89560290347679938, 0.000000000000000000 ) ) ;
#4499=CONICAL_SURFACE ( 'NONE', #6675, 14.92500000000000071, 1.076854957875310381 ) ;
#4500=ORIENTED_EDGE ( 'NONE', *, *, #4121, .T. ) ;
#4511=CIRCLE ( 'NONE', #14106, 17.52499999999999858 ) ;
#4536=DIRECTION ( 'NONE',  ( 0.000000000000000000, 1.000000000000000000, 0.000000000000000000 ) ) ;
#4551=FACE_BOUND ( 'NONE', #8407, .T. ) ;
#4581=EDGE_CURVE ( 'NONE', #15921, #2814, #4797, .T. ) ;
#4590=LINE ( 'NONE', #10002, #381 ) ;
#4620=LINE ( 'NONE', #16469, #12599 ) ;
#4628=CARTESIAN_POINT ( 'NONE',  ( 3.850000000000000089, 0.000000000000000000, 0.000000000000000000 ) ) ;
#4665=EDGE_CURVE ( 'NONE', #1142, #15212, #5061, .T. ) ;
#4688=FACE_OUTER_BOUND ( 'NONE', #810, .T. ) ;
#4710=ORIENTED_EDGE ( 'NONE', *, *, #16927, .F. ) ;
#4719=PRODUCT_CONTEXT ( 'NONE', #7082, 'mechanical' ) ;
#4725=CARTESIAN_POINT ( 'NONE',  ( 7.000000000000000000, 0.000000000000000000, 0.000000000000000000 ) ) ;
#4731=EDGE_LOOP ( 'NONE', ( #13958, #8713, #2598, #8250 ) ) ;
#4735=AXIS2_PLACEMENT_3D ( 'NONE', #16454, #11053, #2026 ) ;
#4746=CIRCLE ( 'NONE', #7209, 17.52499999999999858 ) ;
#4795=CARTESIAN_POINT ( 'NONE',  ( 3.500000000000000000, 14.59999999999999964, 0.000000000000000000 ) ) ;
#4797=CIRCLE ( 'NONE', #425, 17.85000000000000142 ) ;
#4831=AXIS2_PLACEMENT_3D ( 'NONE', #11322, #7191, #12450 ) ;
#4846=CARTESIAN_POINT ( 'NONE',  ( 1.050000000000000044, 0.000000000000000000, 0.000000000000000000 ) ) ;
#4878=CARTESIAN_POINT ( 'NONE',  ( 1.399999999999999911, -15.25000000000000000, -1.867586368699713770E-15 ) ) ;
#4900=EDGE_LOOP ( 'NONE', ( #3063, #16869, #15004, #13150, #1047 ) ) ;
#4907=ORIENTED_EDGE ( 'NONE', *, *, #10062, .T. ) ;
#4915=CIRCLE ( 'NONE', #3003, 13.95000000000000107 ) ;
#4923=CARTESIAN_POINT ( 'NONE',  ( 5.425003271131650706, -12.64814671169700055, 1.549064719741994274E-15 ) ) ;
#4930=AXIS2_PLACEMENT_3D ( 'NONE', #14586, #2815, #8054 ) ;
#4932=AXIS2_PLACEMENT_3D ( 'NONE', #2472, #12956, #7449 ) ;
#4939=ORIENTED_EDGE ( 'NONE', *, *, #16737, .T. ) ;
#4951=LINE ( 'NONE', #2382, #11606 ) ;
#4954=FACE_OUTER_BOUND ( 'NONE', #7585, .T. ) ;
#4983=ORIENTED_EDGE ( 'NONE', *, *, #7120, .F. ) ;
#4998=AXIS2_PLACEMENT_3D ( 'NONE', #11924, #2639, #10630 ) ;
#5001=DIRECTION ( 'NONE',  ( 1.000000000000000000, 0.000000000000000000, 0.000000000000000000 ) ) ;
#5011=ORIENTED_EDGE ( 'NONE', *, *, #12700, .T. ) ;
#5015=AXIS2_PLACEMENT_3D ( 'NONE', #7577, #10346, #15576 ) ;
#5018=CIRCLE ( 'NONE', #4735, 13.95000000000000107 ) ;
#5023=ORIENTED_EDGE ( 'NONE', *, *, #16690, .F. ) ;
#5044=CARTESIAN_POINT ( 'NONE',  ( 3.324999999999999734, 0.000000000000000000, 0.000000000000000000 ) ) ;
#5061=CIRCLE ( 'NONE', #8085, 17.85000000000000142 ) ;
#5072=DIRECTION ( 'NONE',  ( 0.000000000000000000, 1.000000000000000000, 0.000000000000000000 ) ) ;
#5136=DIRECTION ( 'NONE',  ( 1.000000000000000000, 0.000000000000000000, 0.000000000000000000 ) ) ;
#5158=ORIENTED_EDGE ( 'NONE', *, *, #15505, .F. ) ;
#5170=ORIENTED_EDGE ( 'NONE', *, *, #13162, .T. ) ;
#5212=CARTESIAN_POINT ( 'NONE',  ( 0.6999999999999999556, 0.000000000000000000, 0.000000000000000000 ) ) ;
#5220=ORIENTED_EDGE ( 'NONE', *, *, #7376, .T. ) ;
#5232=EDGE_LOOP ( 'NONE', ( #6099, #4087, #13429, #8171, #16045 ) ) ;
#5244=FACE_OUTER_BOUND ( 'NONE', #4900, .T. ) ;
#5252=EDGE_LOOP ( 'NONE', ( #6435, #7413, #11771, #323 ) ) ;
#5282=ADVANCED_FACE ( 'NONE', ( #16530 ), #14693, .T. ) ;
#5287=AXIS2_PLACEMENT_3D ( 'NONE', #3323, #15339, #8402 ) ;
#5326=LINE ( 'NONE', #15810, #7615 ) ;
#5337=ORIENTED_EDGE ( 'NONE', *, *, #15357, .T. ) ;
#5348=FACE_BOUND ( 'NONE', #11004, .T. ) ;
#5370=CARTESIAN_POINT ( 'NONE',  ( 6.649999999999999467, 18.17500000000000071, 0.000000000000000000 ) ) ;
#5388=DIRECTION ( 'NONE',  ( 0.000000000000000000, 1.000000000000000000, 0.000000000000000000 ) ) ;
#5407=DIRECTION ( 'NONE',  ( 0.000000000000000000, 1.000000000000000000, 0.000000000000000000 ) ) ;
#5429=FACE_OUTER_BOUND ( 'NONE', #16389, .T. ) ;
#5445=CARTESIAN_POINT ( 'NONE',  ( 3.324999999999999734, -12.97499999999999964, -1.588979221893690953E-15 ) ) ;
#5450=DIRECTION ( 'NONE',  ( 0.000000000000000000, 1.000000000000000000, 0.000000000000000000 ) ) ;
#5483=DIRECTION ( 'NONE',  ( 0.000000000000000000, 1.000000000000000000, 0.000000000000000000 ) ) ;
#5527=EDGE_LOOP ( 'NONE', ( #10604, #4500, #13711, #7639 ) ) ;
#5534=DIRECTION ( 'NONE',  ( -1.000000000000000000, 0.000000000000000000, 0.000000000000000000 ) ) ;
#5553=ORIENTED_EDGE ( 'NONE', *, *, #13805, .T. ) ;
#5582=DIRECTION ( 'NONE',  ( 1.000000000000000000, 0.000000000000000000, 0.000000000000000000 ) ) ;
#5605=DIRECTION ( 'NONE',  ( -1.000000000000000000, 0.000000000000000000, 0.000000000000000000 ) ) ;
#5631=CARTESIAN_POINT ( 'NONE',  ( 5.044974746830580337, 1.808800229719332446E-15, 14.76997474683059153 ) ) ;
#5634=DIRECTION ( 'NONE',  ( -0.7327934916262990317, 0.6804510993672779895, 0.000000000000000000 ) ) ;
#5635=DIRECTION ( 'NONE',  ( 0.000000000000000000, 0.000000000000000000, -1.000000000000000000 ) ) ;
#5651=EDGE_LOOP ( 'NONE', ( #12650, #4111, #12241, #16091 ) ) ;
#5679=ORIENTED_EDGE ( 'NONE', *, *, #1614, .T. ) ;
#5680=DIRECTION ( 'NONE',  ( 0.000000000000000000, 1.000000000000000000, 0.000000000000000000 ) ) ;
#5683=AXIS2_PLACEMENT_3D ( 'NONE', #4846, #10093, #14038 ) ;
#5704=AXIS2_PLACEMENT_3D ( 'NONE', #3924, #10292, #11557 ) ;
#5710=DIRECTION ( 'NONE',  ( 1.000000000000000000, 0.000000000000000000, 0.000000000000000000 ) ) ;
#5725=EDGE_CURVE ( 'NONE', #11007, #9884, #11676, .T. ) ;
#5770=ORIENTED_EDGE ( 'NONE', *, *, #11071, .T. ) ;
#5784=ADVANCED_FACE ( 'NONE', ( #4551, #13828 ), #8589, .T. ) ;
#5814=DIRECTION ( 'NONE',  ( -1.000000000000000000, 0.000000000000000000, 0.000000000000000000 ) ) ;
#5860=AXIS2_PLACEMENT_3D ( 'NONE', #9327, #5534, #8286 ) ;
#5871=( GEOMETRIC_REPRESENTATION_CONTEXT ( 3 ) GLOBAL_UNCERTAINTY_ASSIGNED_CONTEXT ( ( #1716 ) ) GLOBAL_UNIT_ASSIGNED_CONTEXT ( ( #13062, #7800, #14430 ) ) REPRESENTATION_CONTEXT ( 'NONE', 'WORKASPACE' ) );
#5894=VERTEX_POINT ( 'NONE', #7617 ) ;
#5898=VERTEX_POINT ( 'NONE', #2557 ) ;
#5906=DIRECTION ( 'NONE',  ( 1.000000000000000000, 0.000000000000000000, 0.000000000000000000 ) ) ;
#5914=ORIENTED_EDGE ( 'NONE', *, *, #15357, .F. ) ;
#5924=ORIENTED_EDGE ( 'NONE', *, *, #4581, .F. ) ;
#5933=ADVANCED_FACE ( 'NONE', ( #11414 ), #11687, .F. ) ;
#5949=AXIS2_PLACEMENT_3D ( 'NONE', #8802, #986, #16687 ) ;
#5952=ORIENTED_EDGE ( 'NONE', *, *, #12746, .T. ) ;
#6000=FILL_AREA_STYLE_COLOUR ( '', #7324 ) ;
#6004=DIRECTION ( 'NONE',  ( -1.000000000000000000, 0.000000000000000000, 0.000000000000000000 ) ) ;
#6030=CARTESIAN_POINT ( 'NONE',  ( 1.399999999999999911, 0.000000000000000000, 0.000000000000000000 ) ) ;
#6053=CONICAL_SURFACE ( 'NONE', #14024, 18.17500000000000071, 0.7483780475235185525 ) ;
#6075=ORIENTED_EDGE ( 'NONE', *, *, #16540, .T. ) ;
#6099=ORIENTED_EDGE ( 'NONE', *, *, #2534, .T. ) ;
#6112=CARTESIAN_POINT ( 'NONE',  ( 0.6999999999999999556, 0.000000000000000000, 0.000000000000000000 ) ) ;
#6141=ADVANCED_FACE ( 'NONE', ( #585 ), #15088, .T. ) ;
#6142=PRODUCT_DEFINITION_SHAPE ( 'NONE', 'NONE',  #8102 ) ;
#6149=FACE_OUTER_BOUND ( 'NONE', #15097, .T. ) ;
#6150=CIRCLE ( 'NONE', #4244, 12.65000000000000036 ) ;
#6161=CARTESIAN_POINT ( 'NONE',  ( 1.224999999999999867, -15.25000000000000000, -1.867586368699713770E-15 ) ) ;
#6174=EDGE_CURVE ( 'NONE', #15212, #1142, #6470, .T. ) ;
#6189=VERTEX_POINT ( 'NONE', #3330 ) ;
#6194=DIRECTION ( 'NONE',  ( 0.000000000000000000, 1.000000000000000000, 0.000000000000000000 ) ) ;
#6200=CIRCLE ( 'NONE', #5683, 15.25000000000000000 ) ;
#6207=VERTEX_POINT ( 'NONE', #8570 ) ;
#6209=ORIENTED_EDGE ( 'NONE', *, *, #15086, .F. ) ;
#6212=DIRECTION ( 'NONE',  ( 1.000000000000000000, 0.000000000000000000, 0.000000000000000000 ) ) ;
#6247=DIRECTION ( 'NONE',  ( 0.000000000000000000, 1.000000000000000000, 0.000000000000000000 ) ) ;
#6270=EDGE_LOOP ( 'NONE', ( #9001, #3257 ) ) ;
#6302=CIRCLE ( 'NONE', #11488, 13.29999999999999893 ) ;
#6304=CARTESIAN_POINT ( 'NONE',  ( 2.625000000000000000, 14.59999999999999964, 0.000000000000000000 ) ) ;
#6314=DIRECTION ( 'NONE',  ( 0.9999937692730440641, 0.003530072958125829961, 0.000000000000000000 ) ) ;
#6336=ADVANCED_FACE ( 'NONE', ( #5348, #5429 ), #1492, .T. ) ;
#6351=ORIENTED_EDGE ( 'NONE', *, *, #10552, .T. ) ;
#6362=CONICAL_SURFACE ( 'NONE', #16534, 13.89560290347679938, 1.567266246505109928 ) ;
#6363=CARTESIAN_POINT ( 'NONE',  ( 5.941205806953520074, 0.000000000000000000, 0.000000000000000000 ) ) ;
#6374=ADVANCED_FACE ( 'NONE', ( #15740 ), #11431, .F. ) ;
#6381=EDGE_LOOP ( 'NONE', ( #6710, #12604 ) ) ;
#6383=DIRECTION ( 'NONE',  ( 0.000000000000000000, 1.000000000000000000, 0.000000000000000000 ) ) ;
#6390=AXIS2_PLACEMENT_3D ( 'NONE', #9500, #5710, #141 ) ;
#6435=ORIENTED_EDGE ( 'NONE', *, *, #1939, .F. ) ;
#6442=ORIENTED_EDGE ( 'NONE', *, *, #3271, .F. ) ;
#6451=CARTESIAN_POINT ( 'NONE',  ( 0.6999999999999999556, -18.50000000000000000, -2.265596578422603396E-15 ) ) ;
#6470=CIRCLE ( 'NONE', #7851, 17.85000000000000142 ) ;
#6474=EDGE_CURVE ( 'NONE', #6725, #14628, #2379, .T. ) ;
#6488=DIRECTION ( 'NONE',  ( -1.000000000000000000, 0.000000000000000000, 0.000000000000000000 ) ) ;
#6518=DIRECTION ( 'NONE',  ( -1.000000000000000000, 0.000000000000000000, 0.000000000000000000 ) ) ;
#6530=CARTESIAN_POINT ( 'NONE',  ( 3.850000000000000089, 0.000000000000000000, 0.000000000000000000 ) ) ;
#6532=CARTESIAN_POINT ( 'NONE',  ( 5.569974746830579804, 0.000000000000000000, 0.000000000000000000 ) ) ;
#6537=FACE_OUTER_BOUND ( 'NONE', #7843, .T. ) ;
#6548=ADVANCED_FACE ( 'NONE', ( #12139 ), #2108, .T. ) ;
#6550=CARTESIAN_POINT ( 'NONE',  ( -8.881784197001250351E-16, 17.85000000000000142, 0.000000000000000000 ) ) ;
#6563=CIRCLE ( 'NONE', #8235, 17.52499999999999858 ) ;
#6624=ORIENTED_EDGE ( 'NONE', *, *, #7758, .F. ) ;
#6667=AXIS2_PLACEMENT_3D ( 'NONE', #188, #5582, #8333 ) ;
#6674=DIRECTION ( 'NONE',  ( 1.000000000000000000, 0.000000000000000000, 0.000000000000000000 ) ) ;
#6675=AXIS2_PLACEMENT_3D ( 'NONE', #14120, #8795, #7570 ) ;
#6703=ORIENTED_EDGE ( 'NONE', *, *, #7376, .F. ) ;
#6710=ORIENTED_EDGE ( 'NONE', *, *, #15070, .T. ) ;
#6725=VERTEX_POINT ( 'NONE', #11436 ) ;
#6747=AXIS2_PLACEMENT_3D ( 'NONE', #12095, #335, #14588 ) ;
#6775=DIRECTION ( 'NONE',  ( 1.000000000000000000, 0.000000000000000000, 0.000000000000000000 ) ) ;
#6784=ADVANCED_FACE ( 'NONE', ( #3873 ), #7272, .T. ) ;
#6787=VERTEX_POINT ( 'NONE', #7638 ) ;
#6793=CARTESIAN_POINT ( 'NONE',  ( 0.3499999999999999778, 18.17500000000000071, 0.000000000000000000 ) ) ;
#6810=LINE ( 'NONE', #9321, #14319 ) ;
#6814=CARTESIAN_POINT ( 'NONE',  ( 5.687501635565830327, -12.64907335584850046, 1.549064719741993485E-15 ) ) ;
#6817=CARTESIAN_POINT ( 'NONE',  ( 7.000000000000000000, 0.000000000000000000, 0.000000000000000000 ) ) ;
#6867=EDGE_LOOP ( 'NONE', ( #7497, #14609, #5914, #13154, #6209 ) ) ;
#6876=CARTESIAN_POINT ( 'NONE',  ( 1.050000000000000044, 0.000000000000000000, 0.000000000000000000 ) ) ;
#6929=CONICAL_SURFACE ( 'NONE', #15444, 18.17500000000000071, 0.7483780475235185525 ) ;
#6957=AXIS2_PLACEMENT_3D ( 'NONE', #16836, #6518, #5072 ) ;
#6964=ORIENTED_EDGE ( 'NONE', *, *, #14837, .T. ) ;
#6978=DIRECTION ( 'NONE',  ( 1.000000000000000000, 0.000000000000000000, 0.000000000000000000 ) ) ;
#6994=CARTESIAN_POINT ( 'NONE',  ( 1.050000000000000044, 0.000000000000000000, 0.000000000000000000 ) ) ;
#7011=CARTESIAN_POINT ( 'NONE',  ( 1.224999999999999867, 0.000000000000000000, 0.000000000000000000 ) ) ;
#7016=ORIENTED_EDGE ( 'NONE', *, *, #15708, .F. ) ;
#7032=ORIENTED_EDGE ( 'NONE', *, *, #4132, .T. ) ;
#7055=STYLED_ITEM ( 'NONE', ( #12712 ), #8355 ) ;
#7057=EDGE_LOOP ( 'NONE', ( #14483, #4907, #8310, #13491 ) ) ;
#7068=EDGE_CURVE ( 'NONE', #6189, #793, #16078, .T. ) ;
#7082=APPLICATION_CONTEXT ( 'automotive_design' ) ;
#7096=CARTESIAN_POINT ( 'NONE',  ( 4.025000000000000355, 0.000000000000000000, 0.000000000000000000 ) ) ;
#7109=DIRECTION ( 'NONE',  ( 0.000000000000000000, -1.000000000000000000, 0.000000000000000000 ) ) ;
#7120=EDGE_CURVE ( 'NONE', #11290, #16915, #8120, .T. ) ;
#7155=CLOSED_SHELL ( 'NONE', ( #5282, #1284, #12567, #13700, #5933, #12130, #309, #1079, #7171, #2897, #15658, #14881, #12858, #2654, #6141, #12282, #6336, #5784, #7911, #6784, #16658, #1940, #6548, #8684, #11155, #4322, #6374, #8234, #11716, #12770, #9936, #503, #11584 ) ) ;
#7171=ADVANCED_FACE ( 'NONE', ( #10553 ), #11406, .T. ) ;
#7173=DIRECTION ( 'NONE',  ( 1.000000000000000000, 0.000000000000000000, 0.000000000000000000 ) ) ;
#7191=DIRECTION ( 'NONE',  ( 1.000000000000000000, -6.123031769111888756E-17, 0.000000000000000000 ) ) ;
#7197=CARTESIAN_POINT ( 'NONE',  ( 5.425003271131650706, 0.000000000000000000, 0.000000000000000000 ) ) ;
#7204=EDGE_CURVE ( 'NONE', #6787, #5898, #11834, .T. ) ;
#7207=SHAPE_DEFINITION_REPRESENTATION ( #6142, #7583 ) ;
#7209=AXIS2_PLACEMENT_3D ( 'NONE', #10954, #10783, #16019 ) ;
#7219=DIRECTION ( 'NONE',  ( 0.000000000000000000, 1.224646799147356165E-16, 1.000000000000000000 ) ) ;
#7231=ORIENTED_EDGE ( 'NONE', *, *, #3543, .F. ) ;
#7257=DIRECTION ( 'NONE',  ( 0.000000000000000000, -1.000000000000000000, 0.000000000000000000 ) ) ;
#7264=CARTESIAN_POINT ( 'NONE',  ( 1.399999999999999911, 0.000000000000000000, 0.000000000000000000 ) ) ;
#7265=AXIS2_PLACEMENT_3D ( 'NONE', #3746, #6212, #10181 ) ;
#7271=DIRECTION ( 'NONE',  ( 0.000000000000000000, 1.000000000000000000, 0.000000000000000000 ) ) ;
#7272=CONICAL_SURFACE ( 'NONE', #13370, 18.17500000000000071, 0.7483780475235185525 ) ;
#7318=EDGE_CURVE ( 'NONE', #2563, #199, #9517, .T. ) ;
#7324=COLOUR_RGB ( '', 0.31764706, 0.68627451, 0.89019608) ;
#7352=DIRECTION ( 'NONE',  ( 0.7327934916262990317, -0.6804510993672779895, 8.333122608164345406E-17 ) ) ;
#7376=EDGE_CURVE ( 'NONE', #13527, #16649, #2992, .T. ) ;
#7389=VERTEX_POINT ( 'NONE', #12190 ) ;
#7413=ORIENTED_EDGE ( 'NONE', *, *, #16143, .F. ) ;
#7429=DIRECTION ( 'NONE',  ( -1.000000000000000000, 0.000000000000000000, 0.000000000000000000 ) ) ;
#7449=DIRECTION ( 'NONE',  ( 0.000000000000000000, 1.000000000000000000, 0.000000000000000000 ) ) ;
#7469=VERTEX_POINT ( 'NONE', #8660 ) ;
#7485=CARTESIAN_POINT ( 'NONE',  ( 3.850000000000000089, 0.000000000000000000, 0.000000000000000000 ) ) ;
#7487=EDGE_CURVE ( 'NONE', #199, #2563, #15542, .T. ) ;
#7497=ORIENTED_EDGE ( 'NONE', *, *, #1087, .T. ) ;
#7570=DIRECTION ( 'NONE',  ( 0.000000000000000000, 1.000000000000000000, 0.000000000000000000 ) ) ;
#7577=CARTESIAN_POINT ( 'NONE',  ( 3.850000000000000089, 0.000000000000000000, 0.000000000000000000 ) ) ;
#7578=ORIENTED_EDGE ( 'NONE', *, *, #404, .F. ) ;
#7583=SHAPE_REPRESENTATION ( '722909', ( #1488 ), #5871 ) ;
#7585=EDGE_LOOP ( 'NONE', ( #2018, #13763, #2467, #8936, #12058 ) ) ;
#7614=ORIENTED_EDGE ( 'NONE', *, *, #10552, .F. ) ;
#7615=VECTOR ( 'NONE', #8334, 1000.000000000000000 ) ;
#7617=CARTESIAN_POINT ( 'NONE',  ( 3.850000000000000089, 1.778491767751089605E-15, 14.27500000000000036 ) ) ;
#7625=DIRECTION ( 'NONE',  ( 0.000000000000000000, 0.000000000000000000, -1.000000000000000000 ) ) ;
#7638=CARTESIAN_POINT ( 'NONE',  ( 2.799999999999999822, 13.30000000000000071, 0.000000000000000000 ) ) ;
#7639=ORIENTED_EDGE ( 'NONE', *, *, #7204, .F. ) ;
#7653=DIRECTION ( 'NONE',  ( 1.000000000000000000, 0.000000000000000000, 0.000000000000000000 ) ) ;
#7717=VERTEX_POINT ( 'NONE', #10787 ) ;
#7739=DIRECTION ( 'NONE',  ( 0.000000000000000000, 0.000000000000000000, -1.000000000000000000 ) ) ;
#7742=DIRECTION ( 'NONE',  ( 0.000000000000000000, 1.000000000000000000, 0.000000000000000000 ) ) ;
#7758=EDGE_CURVE ( 'NONE', #15921, #2563, #12167, .T. ) ;
#7764=AXIS2_PLACEMENT_3D ( 'NONE', #7978, #15882, #12034 ) ;
#7800=( NAMED_UNIT ( * ) PLANE_ANGLE_UNIT ( ) SI_UNIT ( $, .RADIAN. ) );
#7843=EDGE_LOOP ( 'NONE', ( #13592, #10774, #13364, #6624 ) ) ;
#7850=EDGE_LOOP ( 'NONE', ( #1742, #5170 ) ) ;
#7851=AXIS2_PLACEMENT_3D ( 'NONE', #9859, #10972, #12594 ) ;
#7852=DIRECTION ( 'NONE',  ( 0.000000000000000000, 1.000000000000000000, 0.000000000000000000 ) ) ;
#7872=MECHANICAL_DESIGN_GEOMETRIC_PRESENTATION_REPRESENTATION('',(#7055),#212);
#7895=DIRECTION ( 'NONE',  ( 1.000000000000000000, 0.000000000000000000, 0.000000000000000000 ) ) ;
#7911=ADVANCED_FACE ( 'NONE', ( #8641 ), #2101, .T. ) ;
#7914=CARTESIAN_POINT ( 'NONE',  ( 5.687501635565830327, 0.000000000000000000, 0.000000000000000000 ) ) ;
#7978=CARTESIAN_POINT ( 'NONE',  ( -1.776356839400249676E-15, 15.90000000000000036, 0.000000000000000000 ) ) ;
#7989=EDGE_CURVE ( 'NONE', #11248, #14244, #11989, .T. ) ;
#8018=VERTEX_POINT ( 'NONE', #6451 ) ;
#8019=CARTESIAN_POINT ( 'NONE',  ( 0.3499999999999999778, 0.000000000000000000, 0.000000000000000000 ) ) ;
#8032=AXIS2_PLACEMENT_3D ( 'NONE', #9045, #14283, #13001 ) ;
#8039=CIRCLE ( 'NONE', #8872, 14.76997474683060041 ) ;
#8040=VECTOR ( 'NONE', #3751, 1000.000000000000114 ) ;
#8043=EDGE_CURVE ( 'NONE', #7717, #16161, #6200, .T. ) ;
#8051=AXIS2_PLACEMENT_3D ( 'NONE', #6994, #12248, #14907 ) ;
#8054=DIRECTION ( 'NONE',  ( 0.000000000000000000, 1.224646799147356165E-16, 1.000000000000000000 ) ) ;
#8085=AXIS2_PLACEMENT_3D ( 'NONE', #13735, #516, #7271 ) ;
#8088=EDGE_CURVE ( 'NONE', #2563, #7469, #384, .T. ) ;
#8102=PRODUCT_DEFINITION ( 'UNKNOWN', '', #3984, #434 ) ;
#8105=DIRECTION ( 'NONE',  ( -0.003530072958128175308, -0.9999937692730440641, -1.224639168707530015E-16 ) ) ;
#8114=DIRECTION ( 'NONE',  ( -0.7327934916262990317, -0.6804510993672779895, -8.333122608164345406E-17 ) ) ;
#8120=CIRCLE ( 'NONE', #2351, 14.59999999999999964 ) ;
#8169=EDGE_LOOP ( 'NONE', ( #13421, #14187, #8585, #7578 ) ) ;
#8171=ORIENTED_EDGE ( 'NONE', *, *, #11071, .F. ) ;
#8184=DIRECTION ( 'NONE',  ( 0.000000000000000000, 1.000000000000000000, 0.000000000000000000 ) ) ;
#8233=DIRECTION ( 'NONE',  ( 0.000000000000000000, 1.000000000000000000, 0.000000000000000000 ) ) ;
#8234=ADVANCED_FACE ( 'NONE', ( #10941 ), #13104, .F. ) ;
#8235=AXIS2_PLACEMENT_3D ( 'NONE', #14684, #166, #5388 ) ;
#8250=ORIENTED_EDGE ( 'NONE', *, *, #4342, .F. ) ;
#8286=DIRECTION ( 'NONE',  ( 0.000000000000000000, 1.000000000000000000, 0.000000000000000000 ) ) ;
#8310=ORIENTED_EDGE ( 'NONE', *, *, #13151, .F. ) ;
#8311=CARTESIAN_POINT ( 'NONE',  ( 5.941205806953520074, 0.000000000000000000, 0.000000000000000000 ) ) ;
#8321=ORIENTED_EDGE ( 'NONE', *, *, #589, .F. ) ;
#8333=DIRECTION ( 'NONE',  ( 0.000000000000000000, 1.000000000000000000, 0.000000000000000000 ) ) ;
#8334=DIRECTION ( 'NONE',  ( -1.000000000000000000, 0.000000000000000000, 0.000000000000000000 ) ) ;
#8337=CONICAL_SURFACE ( 'NONE', #10526, 12.32407335584850117, 0.8899833664651138898 ) ;
#8355=MANIFOLD_SOLID_BREP ( 'Imported1', #7155 ) ;
#8360=ORIENTED_EDGE ( 'NONE', *, *, #15708, .T. ) ;
#8366=VECTOR ( 'NONE', #11582, 1000.000000000000000 ) ;
#8384=DIRECTION ( 'NONE',  ( -0.8502651466878615727, -0.5263546146162958461, -6.445984940062853155E-17 ) ) ;
#8401=DIRECTION ( 'NONE',  ( 0.000000000000000000, 1.000000000000000000, 0.000000000000000000 ) ) ;
#8402=DIRECTION ( 'NONE',  ( 0.000000000000000000, 1.000000000000000000, 0.000000000000000000 ) ) ;
#8407=EDGE_LOOP ( 'NONE', ( #5023, #3898 ) ) ;
#8422=CARTESIAN_POINT ( 'NONE',  ( 4.549999999999999822, 0.000000000000000000, -14.27500000000000036 ) ) ;
#8426=AXIS2_PLACEMENT_3D ( 'NONE', #210, #1315, #30 ) ;
#8450=CARTESIAN_POINT ( 'NONE',  ( 5.945602903476760126, 0.000000000000000000, 0.000000000000000000 ) ) ;
#8469=CARTESIAN_POINT ( 'NONE',  ( 3.500000000000000000, 0.000000000000000000, 0.000000000000000000 ) ) ;
#8496=LINE ( 'NONE', #3180, #9319 ) ;
#8505=DIRECTION ( 'NONE',  ( 1.000000000000000000, 0.000000000000000000, 0.000000000000000000 ) ) ;
#8510=FACE_OUTER_BOUND ( 'NONE', #8945, .T. ) ;
#8529=EDGE_CURVE ( 'NONE', #1142, #8018, #16053, .T. ) ;
#8547=CIRCLE ( 'NONE', #15124, 18.50000000000000000 ) ;
#8570=CARTESIAN_POINT ( 'NONE',  ( 3.850000000000000089, 14.27500000000000036, 0.000000000000000000 ) ) ;
#8585=ORIENTED_EDGE ( 'NONE', *, *, #7120, .T. ) ;
#8589=PLANE ( 'NONE',  #4831 ) ;
#8620=ORIENTED_EDGE ( 'NONE', *, *, #15067, .T. ) ;
#8629=CARTESIAN_POINT ( 'NONE',  ( 1.399999999999999911, 15.25000000000000000, 0.000000000000000000 ) ) ;
#8641=FACE_OUTER_BOUND ( 'NONE', #3884, .T. ) ;
#8660=CARTESIAN_POINT ( 'NONE',  ( 0.6999999999999999556, 18.50000000000000000, 0.000000000000000000 ) ) ;
#8684=ADVANCED_FACE ( 'NONE', ( #16794 ), #4014, .T. ) ;
#8693=DIRECTION ( 'NONE',  ( 0.000000000000000000, 0.000000000000000000, 1.000000000000000000 ) ) ;
#8713=ORIENTED_EDGE ( 'NONE', *, *, #11192, .T. ) ;
#8718=AXIS2_PLACEMENT_3D ( 'NONE', #2064, #6978, #13921 ) ;
#8740=ORIENTED_EDGE ( 'NONE', *, *, #3271, .T. ) ;
#8750=DIRECTION ( 'NONE',  ( -1.000000000000000000, 0.000000000000000000, 0.000000000000000000 ) ) ;
#8762=PRODUCT ( '722909', '722909', '', ( #4719 ) ) ;
#8765=ORIENTED_EDGE ( 'NONE', *, *, #15774, .T. ) ;
#8795=DIRECTION ( 'NONE',  ( -1.000000000000000000, 0.000000000000000000, 0.000000000000000000 ) ) ;
#8802=CARTESIAN_POINT ( 'NONE',  ( 1.399999999999999911, 0.000000000000000000, 0.000000000000000000 ) ) ;
#8846=DIRECTION ( 'NONE',  ( 0.000000000000000000, 1.000000000000000000, 0.000000000000000000 ) ) ;
#8850=APPLICATION_CONTEXT ( 'automotive_design' ) ;
#8872=AXIS2_PLACEMENT_3D ( 'NONE', #12800, #15370, #8846 ) ;
#8886=DIRECTION ( 'NONE',  ( 0.000000000000000000, 1.000000000000000000, 0.000000000000000000 ) ) ;
#8936=ORIENTED_EDGE ( 'NONE', *, *, #589, .T. ) ;
#8945=EDGE_LOOP ( 'NONE', ( #14047, #15164, #5220, #5337, #15517 ) ) ;
#9001=ORIENTED_EDGE ( 'NONE', *, *, #6174, .F. ) ;
#9012=VERTEX_POINT ( 'NONE', #16447 ) ;
#9045=CARTESIAN_POINT ( 'NONE',  ( 3.324999999999999734, 0.000000000000000000, 0.000000000000000000 ) ) ;
#9057=AXIS2_PLACEMENT_3D ( 'NONE', #10128, #10382, #3853 ) ;
#9124=VECTOR ( 'NONE', #234, 1000.000000000000000 ) ;
#9129=AXIS2_PLACEMENT_3D ( 'NONE', #2302, #6488, #11487 ) ;
#9155=CARTESIAN_POINT ( 'NONE',  ( 3.324999999999999734, 12.97499999999999964, 0.000000000000000000 ) ) ;
#9158=CARTESIAN_POINT ( 'NONE',  ( 4.899999999999999467, 0.000000000000000000, 0.000000000000000000 ) ) ;
#9221=ORIENTED_EDGE ( 'NONE', *, *, #15505, .T. ) ;
#9230=CARTESIAN_POINT ( 'NONE',  ( 5.162501635565829972, -12.32407335584850117, 1.509263698769704680E-15 ) ) ;
#9232=CARTESIAN_POINT ( 'NONE',  ( 3.500000000000000000, 18.50000000000000000, 0.000000000000000000 ) ) ;
#9245=ORIENTED_EDGE ( 'NONE', *, *, #1523, .F. ) ;
#9255=ORIENTED_EDGE ( 'NONE', *, *, #15185, .T. ) ;
#9261=ORIENTED_EDGE ( 'NONE', *, *, #7318, .T. ) ;
#9319=VECTOR ( 'NONE', #15276, 1000.000000000000000 ) ;
#9321=CARTESIAN_POINT ( 'NONE',  ( 1.574999999999999956, 14.92500000000000071, 0.000000000000000000 ) ) ;
#9327=CARTESIAN_POINT ( 'NONE',  ( 4.025000000000000355, 0.000000000000000000, 0.000000000000000000 ) ) ;
#9342=AXIS2_PLACEMENT_3D ( 'NONE', #6817, #14486, #13458 ) ;
#9379=AXIS2_PLACEMENT_3D ( 'NONE', #3781, #5136, #7625 ) ;
#9408=VECTOR ( 'NONE', #8105, 1000.000000000000227 ) ;
#9452=ORIENTED_EDGE ( 'NONE', *, *, #3232, .F. ) ;
#9476=DIRECTION ( 'NONE',  ( 0.000000000000000000, 1.000000000000000000, 0.000000000000000000 ) ) ;
#9486=CARTESIAN_POINT ( 'NONE',  ( 5.945602903476760126, -13.89560290347679938, -1.701720561796553076E-15 ) ) ;
#9492=AXIS2_PLACEMENT_3D ( 'NONE', #376, #5605, #13762 ) ;
#9500=CARTESIAN_POINT ( 'NONE',  ( 5.941205806953520074, 0.000000000000000000, 0.000000000000000000 ) ) ;
#9517=CIRCLE ( 'NONE', #6747, 18.50000000000000000 ) ;
#9520=AXIS2_PLACEMENT_3D ( 'NONE', #7914, #14056, #1398 ) ;
#9555=CARTESIAN_POINT ( 'NONE',  ( 1.399999999999999911, -13.62500000000000000, -1.668581263838268760E-15 ) ) ;
#9610=CARTESIAN_POINT ( 'NONE',  ( 6.299999999999999822, -18.50000000000000000, -2.265596578422603396E-15 ) ) ;
#9617=CARTESIAN_POINT ( 'NONE',  ( 7.000000000000000000, 0.000000000000000000, 0.000000000000000000 ) ) ;
#9646=CIRCLE ( 'NONE', #2220, 15.25000000000000000 ) ;
#9723=EDGE_LOOP ( 'NONE', ( #16261, #805, #5011, #11231, #6703 ) ) ;
#9737=EDGE_CURVE ( 'NONE', #13073, #155, #11269, .T. ) ;
#9762=DIRECTION ( 'NONE',  ( -0.4740998230350218501, -0.8804710999221728729, -1.078266114261438272E-16 ) ) ;
#9779=CARTESIAN_POINT ( 'NONE',  ( 5.569974746830579804, 0.000000000000000000, -14.76997474683060041 ) ) ;
#9806=CARTESIAN_POINT ( 'NONE',  ( 1.750000000000000000, 0.000000000000000000, 0.000000000000000000 ) ) ;
#9854=CARTESIAN_POINT ( 'NONE',  ( 5.941205806953520074, -15.14120580695428764, -1.854262922671788806E-15 ) ) ;
#9859=CARTESIAN_POINT ( 'NONE',  ( -8.881784197001250351E-16, 0.000000000000000000, 0.000000000000000000 ) ) ;
#9884=VERTEX_POINT ( 'NONE', #9854 ) ;
#9936=ADVANCED_FACE ( 'NONE', ( #1333 ), #6053, .T. ) ;
#10002=CARTESIAN_POINT ( 'NONE',  ( 1.574999999999999956, -14.92500000000000071, -1.827785347727424768E-15 ) ) ;
#10025=UNCERTAINTY_MEASURE_WITH_UNIT (LENGTH_MEASURE( 1.000000000000000082E-05 ), #1452, 'distance_accuracy_value', 'NONE');
#10057=ORIENTED_EDGE ( 'NONE', *, *, #12760, .F. ) ;
#10062=EDGE_CURVE ( 'NONE', #11116, #3377, #12070, .T. ) ;
#10078=VECTOR ( 'NONE', #33, 1000.000000000000000 ) ;
#10093=DIRECTION ( 'NONE',  ( 1.000000000000000000, 0.000000000000000000, 0.000000000000000000 ) ) ;
#10105=ORIENTED_EDGE ( 'NONE', *, *, #6174, .T. ) ;
#10113=CARTESIAN_POINT ( 'NONE',  ( 5.687501635565830327, 0.000000000000000000, 0.000000000000000000 ) ) ;
#10128=CARTESIAN_POINT ( 'NONE',  ( 0.3499999999999999778, 0.000000000000000000, 0.000000000000000000 ) ) ;
#10156=ORIENTED_EDGE ( 'NONE', *, *, #10365, .T. ) ;
#10181=DIRECTION ( 'NONE',  ( 0.000000000000000000, 0.000000000000000000, -1.000000000000000000 ) ) ;
#10196=LINE ( 'NONE', #12934, #16038 ) ;
#10238=ORIENTED_EDGE ( 'NONE', *, *, #11360, .F. ) ;
#10247=EDGE_CURVE ( 'NONE', #14244, #11248, #9646, .T. ) ;
#10274=EDGE_CURVE ( 'NONE', #7469, #8018, #15119, .T. ) ;
#10292=DIRECTION ( 'NONE',  ( -1.000000000000000000, 0.000000000000000000, 0.000000000000000000 ) ) ;
#10346=DIRECTION ( 'NONE',  ( 1.000000000000000000, 0.000000000000000000, 0.000000000000000000 ) ) ;
#10365=EDGE_CURVE ( 'NONE', #10651, #7389, #2601, .T. ) ;
#10382=DIRECTION ( 'NONE',  ( 1.000000000000000000, 0.000000000000000000, 0.000000000000000000 ) ) ;
#10418=LINE ( 'NONE', #9230, #12987 ) ;
#10429=ORIENTED_EDGE ( 'NONE', *, *, #13721, .T. ) ;
#10481=CONICAL_SURFACE ( 'NONE', #10750, 12.64907335584850046, 0.003530080289784348537 ) ;
#10526=AXIS2_PLACEMENT_3D ( 'NONE', #16913, #7895, #15808 ) ;
#10536=ORIENTED_EDGE ( 'NONE', *, *, #8529, .F. ) ;
#10545=AXIS2_PLACEMENT_3D ( 'NONE', #11947, #6775, #5483 ) ;
#10552=EDGE_CURVE ( 'NONE', #16161, #7717, #12128, .T. ) ;
#10553=FACE_OUTER_BOUND ( 'NONE', #1590, .T. ) ;
#10604=ORIENTED_EDGE ( 'NONE', *, *, #13151, .T. ) ;
#10630=DIRECTION ( 'NONE',  ( 0.000000000000000000, 1.000000000000000000, 0.000000000000000000 ) ) ;
#10651=VERTEX_POINT ( 'NONE', #15043 ) ;
#10689=DIRECTION ( 'NONE',  ( -0.4740998230350218501, 0.8804710999221728729, 0.000000000000000000 ) ) ;
#10748=CIRCLE ( 'NONE', #2515, 12.00000000000000000 ) ;
#10750=AXIS2_PLACEMENT_3D ( 'NONE', #10113, #5906, #16305 ) ;
#10774=ORIENTED_EDGE ( 'NONE', *, *, #14213, .T. ) ;
#10783=DIRECTION ( 'NONE',  ( 1.000000000000000000, 0.000000000000000000, 0.000000000000000000 ) ) ;
#10787=CARTESIAN_POINT ( 'NONE',  ( 1.050000000000000044, -15.25000000000000000, -1.867586368699713770E-15 ) ) ;
#10789=AXIS2_PLACEMENT_3D ( 'NONE', #6532, #7653, #7739 ) ;
#10874=CYLINDRICAL_SURFACE ( 'NONE', #5860, 17.52499999999999858 ) ;
#10875=AXIS2_PLACEMENT_3D ( 'NONE', #7197, #3269, #702 ) ;
#10891=DIRECTION ( 'NONE',  ( -1.000000000000000000, 0.000000000000000000, 0.000000000000000000 ) ) ;
#10941=FACE_OUTER_BOUND ( 'NONE', #14349, .T. ) ;
#10954=CARTESIAN_POINT ( 'NONE',  ( 7.000000000000000000, 0.000000000000000000, 0.000000000000000000 ) ) ;
#10962=ORIENTED_EDGE ( 'NONE', *, *, #10247, .F. ) ;
#10972=DIRECTION ( 'NONE',  ( 1.000000000000000000, 0.000000000000000000, 0.000000000000000000 ) ) ;
#10999=CYLINDRICAL_SURFACE ( 'NONE', #13408, 15.25000000000000000 ) ;
#11004=EDGE_LOOP ( 'NONE', ( #7614, #13210 ) ) ;
#11007=VERTEX_POINT ( 'NONE', #13580 ) ;
#11014=CARTESIAN_POINT ( 'NONE',  ( 7.000000000000000000, 17.85000000000000142, 0.000000000000000000 ) ) ;
#11053=DIRECTION ( 'NONE',  ( 1.000000000000000000, 0.000000000000000000, 0.000000000000000000 ) ) ;
#11060=DIRECTION ( 'NONE',  ( 0.000000000000000000, 1.000000000000000000, 0.000000000000000000 ) ) ;
#11071=EDGE_CURVE ( 'NONE', #12856, #155, #13229, .T. ) ;
#11083=DIRECTION ( 'NONE',  ( 1.000000000000000000, 0.000000000000000000, 0.000000000000000000 ) ) ;
#11116=VERTEX_POINT ( 'NONE', #692 ) ;
#11140=ORIENTED_EDGE ( 'NONE', *, *, #11360, .T. ) ;
#11144=CARTESIAN_POINT ( 'NONE',  ( 3.500000000000000000, 0.000000000000000000, 0.000000000000000000 ) ) ;
#11152=AXIS2_PLACEMENT_3D ( 'NONE', #3253, #7173, #843 ) ;
#11155=ADVANCED_FACE ( 'NONE', ( #4954 ), #13792, .T. ) ;
#11192=EDGE_CURVE ( 'NONE', #11248, #7717, #1098, .T. ) ;
#11206=ORIENTED_EDGE ( 'NONE', *, *, #15895, .T. ) ;
#11231=ORIENTED_EDGE ( 'NONE', *, *, #2477, .T. ) ;
#11246=SURFACE_STYLE_FILL_AREA ( #14890 ) ;
#11248=VERTEX_POINT ( 'NONE', #4878 ) ;
#11250=AXIS2_PLACEMENT_3D ( 'NONE', #7264, #16460, #3332 ) ;
#11269=CIRCLE ( 'NONE', #849, 14.76997474683060041 ) ;
#11290=VERTEX_POINT ( 'NONE', #14415 ) ;
#11306=FACE_OUTER_BOUND ( 'NONE', #15790, .T. ) ;
#11322=CARTESIAN_POINT ( 'NONE',  ( 7.000000000000000000, 17.68750000000000000, 0.000000000000000000 ) ) ;
#11360=EDGE_CURVE ( 'NONE', #3377, #6787, #12419, .T. ) ;
#11406=CONICAL_SURFACE ( 'NONE', #12251, 14.43750000000000000, 0.7483780475235185525 ) ;
#11414=FACE_OUTER_BOUND ( 'NONE', #7057, .T. ) ;
#11431=CONICAL_SURFACE ( 'NONE', #9520, 12.64907335584850046, 0.003530080289784348537 ) ;
#11436=CARTESIAN_POINT ( 'NONE',  ( 3.500000000000000000, -14.59999999999999964, -1.787984326755135766E-15 ) ) ;
#11476=LINE ( 'NONE', #6304, #14318 ) ;
#11487=DIRECTION ( 'NONE',  ( 0.000000000000000000, 1.000000000000000000, 0.000000000000000000 ) ) ;
#11488=AXIS2_PLACEMENT_3D ( 'NONE', #1679, #13112, #5450 ) ;
#11493=DIRECTION ( 'NONE',  ( -1.000000000000000000, 0.000000000000000000, 0.000000000000000000 ) ) ;
#11519=ORIENTED_EDGE ( 'NONE', *, *, #8088, .T. ) ;
#11549=DIRECTION ( 'NONE',  ( 1.000000000000000000, 0.000000000000000000, 0.000000000000000000 ) ) ;
#11555=DIRECTION ( 'NONE',  ( -1.000000000000000000, 0.000000000000000000, 0.000000000000000000 ) ) ;
#11557=DIRECTION ( 'NONE',  ( 0.000000000000000000, 1.000000000000000000, 0.000000000000000000 ) ) ;
#11582=DIRECTION ( 'NONE',  ( -1.000000000000000000, 0.000000000000000000, 0.000000000000000000 ) ) ;
#11584=ADVANCED_FACE ( 'NONE', ( #5244 ), #14623, .T. ) ;
#11597=CARTESIAN_POINT ( 'NONE',  ( 6.649999999999999467, 0.000000000000000000, 0.000000000000000000 ) ) ;
#11606=VECTOR ( 'NONE', #6314, 1000.000000000000227 ) ;
#11615=FACE_OUTER_BOUND ( 'NONE', #586, .T. ) ;
#11624=DIRECTION ( 'NONE',  ( 1.000000000000000000, 0.000000000000000000, 0.000000000000000000 ) ) ;
#11637=ORIENTED_EDGE ( 'NONE', *, *, #2005, .F. ) ;
#11643=VERTEX_POINT ( 'NONE', #2423 ) ;
#11664=ORIENTED_EDGE ( 'NONE', *, *, #4665, .T. ) ;
#11676=CIRCLE ( 'NONE', #991, 15.14120580695350071 ) ;
#11687=CONICAL_SURFACE ( 'NONE', #2918, 12.97499999999999964, 0.5543074962015517304 ) ;
#11688=FACE_OUTER_BOUND ( 'NONE', #5651, .T. ) ;
#11689=DIRECTION ( 'NONE',  ( -1.000000000000000000, 0.000000000000000000, 0.000000000000000000 ) ) ;
#11716=ADVANCED_FACE ( 'NONE', ( #15494 ), #14912, .F. ) ;
#11771=ORIENTED_EDGE ( 'NONE', *, *, #404, .T. ) ;
#11834=LINE ( 'NONE', #16895, #15791 ) ;
#11836=AXIS2_PLACEMENT_3D ( 'NONE', #6876, #12223, #9476 ) ;
#11861=VECTOR ( 'NONE', #1026, 1000.000000000000000 ) ;
#11915=EDGE_CURVE ( 'NONE', #13073, #11007, #12442, .T. ) ;
#11924=CARTESIAN_POINT ( 'NONE',  ( 2.799999999999999822, 0.000000000000000000, 0.000000000000000000 ) ) ;
#11947=CARTESIAN_POINT ( 'NONE',  ( 3.500000000000000000, 0.000000000000000000, 0.000000000000000000 ) ) ;
#11967=DIRECTION ( 'NONE',  ( 1.000000000000000000, 0.000000000000000000, 0.000000000000000000 ) ) ;
#11989=CIRCLE ( 'NONE', #5949, 15.25000000000000000 ) ;
#12034=DIRECTION ( 'NONE',  ( 0.000000000000000000, 0.000000000000000000, 1.000000000000000000 ) ) ;
#12046=EDGE_LOOP ( 'NONE', ( #12683, #16441, #8740, #14149 ) ) ;
#12058=ORIENTED_EDGE ( 'NONE', *, *, #16143, .T. ) ;
#12070=LINE ( 'NONE', #5445, #3882 ) ;
#12095=CARTESIAN_POINT ( 'NONE',  ( 6.299999999999999822, 0.000000000000000000, 0.000000000000000000 ) ) ;
#12113=CARTESIAN_POINT ( 'NONE',  ( 5.941205806953520074, 0.000000000000000000, 0.000000000000000000 ) ) ;
#12128=CIRCLE ( 'NONE', #11836, 15.25000000000000000 ) ;
#12130=ADVANCED_FACE ( 'NONE', ( #11688 ), #8337, .F. ) ;
#12139=FACE_OUTER_BOUND ( 'NONE', #13987, .T. ) ;
#12167=LINE ( 'NONE', #5370, #15008 ) ;
#12190=CARTESIAN_POINT ( 'NONE',  ( 1.050000000000000044, 17.52499999999999858, 0.000000000000000000 ) ) ;
#12196=EDGE_CURVE ( 'NONE', #793, #6189, #1471, .T. ) ;
#12223=DIRECTION ( 'NONE',  ( 1.000000000000000000, 0.000000000000000000, 0.000000000000000000 ) ) ;
#12236=ORIENTED_EDGE ( 'NONE', *, *, #14213, .F. ) ;
#12241=ORIENTED_EDGE ( 'NONE', *, *, #12196, .T. ) ;
#12248=DIRECTION ( 'NONE',  ( 1.000000000000000000, 0.000000000000000000, 0.000000000000000000 ) ) ;
#12251=AXIS2_PLACEMENT_3D ( 'NONE', #14330, #81, #3855 ) ;
#12266=AXIS2_PLACEMENT_3D ( 'NONE', #11144, #12346, #4536 ) ;
#12282=ADVANCED_FACE ( 'NONE', ( #353, #13495 ), #1720, .T. ) ;
#12292=EDGE_LOOP ( 'NONE', ( #10057, #8765, #4229, #5770, #16240 ) ) ;
#12311=ORIENTED_EDGE ( 'NONE', *, *, #7068, .T. ) ;
#12346=DIRECTION ( 'NONE',  ( -1.000000000000000000, 0.000000000000000000, 0.000000000000000000 ) ) ;
#12370=CARTESIAN_POINT ( 'NONE',  ( 5.941205806953520074, 0.000000000000000000, -15.14120580695351670 ) ) ;
#12375=VERTEX_POINT ( 'NONE', #12370 ) ;
#12384=DIRECTION ( 'NONE',  ( 0.000000000000000000, 1.000000000000000000, 0.000000000000000000 ) ) ;
#12397=TOROIDAL_SURFACE ( 'NONE', #16774, 14.27500000000000036, 0.6999999999999999556 ) ;
#12419=CIRCLE ( 'NONE', #4998, 13.29999999999999893 ) ;
#12438=AXIS2_PLACEMENT_3D ( 'NONE', #7011, #10891, #4366 ) ;
#12442=CIRCLE ( 'NONE', #2568, 0.5249999999999994671 ) ;
#12450=DIRECTION ( 'NONE',  ( -6.123031769111888756E-17, -1.000000000000000000, 0.000000000000000000 ) ) ;
#12457=ORIENTED_EDGE ( 'NONE', *, *, #14219, .F. ) ;
#12538=DIRECTION ( 'NONE',  ( 0.000000000000000000, 1.000000000000000000, 0.000000000000000000 ) ) ;
#12567=ADVANCED_FACE ( 'NONE', ( #2306 ), #3034, .T. ) ;
#12594=DIRECTION ( 'NONE',  ( 0.000000000000000000, 1.000000000000000000, 0.000000000000000000 ) ) ;
#12599=VECTOR ( 'NONE', #16312, 1000.000000000000000 ) ;
#12604=ORIENTED_EDGE ( 'NONE', *, *, #13612, .T. ) ;
#12650=ORIENTED_EDGE ( 'NONE', *, *, #16540, .F. ) ;
#12683=ORIENTED_EDGE ( 'NONE', *, *, #7487, .F. ) ;
#12700=EDGE_CURVE ( 'NONE', #9884, #12375, #15636, .T. ) ;
#12712=PRESENTATION_STYLE_ASSIGNMENT (( #14083 ) ) ;
#12719=CIRCLE ( 'NONE', #14919, 14.27500000000000036 ) ;
#12743=CIRCLE ( 'NONE', #10545, 14.59999999999999964 ) ;
#12746=EDGE_CURVE ( 'NONE', #7389, #2600, #6563, .T. ) ;
#12760=EDGE_CURVE ( 'NONE', #5894, #13073, #4401, .T. ) ;
#12770=ADVANCED_FACE ( 'NONE', ( #11306 ), #1657, .F. ) ;
#12787=EDGE_LOOP ( 'NONE', ( #10105, #16395, #3548, #7016 ) ) ;
#12800=CARTESIAN_POINT ( 'NONE',  ( 5.044974746830580337, 0.000000000000000000, 0.000000000000000000 ) ) ;
#12832=DIRECTION ( 'NONE',  ( 0.6294249519366466039, -0.7770612780724246438, 9.516256069327462658E-17 ) ) ;
#12856=VERTEX_POINT ( 'NONE', #3172 ) ;
#12858=ADVANCED_FACE ( 'NONE', ( #4688 ), #16302, .F. ) ;
#12934=CARTESIAN_POINT ( 'NONE',  ( 3.500000000000000000, -18.50000000000000000, -2.265596578422603396E-15 ) ) ;
#12956=DIRECTION ( 'NONE',  ( 1.000000000000000000, 0.000000000000000000, 0.000000000000000000 ) ) ;
#12987=VECTOR ( 'NONE', #12832, 1000.000000000000000 ) ;
#12989=AXIS2_PLACEMENT_3D ( 'NONE', #9158, #11549, #6383 ) ;
#13001=DIRECTION ( 'NONE',  ( 0.000000000000000000, 1.000000000000000000, 0.000000000000000000 ) ) ;
#13042=ORIENTED_EDGE ( 'NONE', *, *, #11192, .F. ) ;
#13056=ADVANCED_BREP_SHAPE_REPRESENTATION ( '', ( #8355, #1488 ), #5871 ) ;
#13062=( LENGTH_UNIT ( ) NAMED_UNIT ( * ) SI_UNIT ( .MILLI., .METRE. ) );
#13066=CARTESIAN_POINT ( 'NONE',  ( 1.050000000000000044, 15.25000000000000000, 0.000000000000000000 ) ) ;
#13073=VERTEX_POINT ( 'NONE', #5631 ) ;
#13104=CONICAL_SURFACE ( 'NONE', #8718, 12.32407335584850117, 0.8899833664651138898 ) ;
#13112=DIRECTION ( 'NONE',  ( 1.000000000000000000, 0.000000000000000000, 0.000000000000000000 ) ) ;
#13132=DIRECTION ( 'NONE',  ( -0.9740972002433518906, 0.2261297071993489949, 0.000000000000000000 ) ) ;
#13138=SHAPE_REPRESENTATION_RELATIONSHIP ( 'NONE' , 'NONE' ,  #7583, #13056 ) ;
#13150=ORIENTED_EDGE ( 'NONE', *, *, #12700, .F. ) ;
#13151=EDGE_CURVE ( 'NONE', #6787, #3377, #6302, .T. ) ;
#13154=ORIENTED_EDGE ( 'NONE', *, *, #2477, .F. ) ;
#13162=EDGE_CURVE ( 'NONE', #2814, #15921, #1348, .T. ) ;
#13210=ORIENTED_EDGE ( 'NONE', *, *, #8043, .F. ) ;
#13229=CIRCLE ( 'NONE', #77, 0.6999999999999992895 ) ;
#13235=ORIENTED_EDGE ( 'NONE', *, *, #16737, .F. ) ;
#13316=CARTESIAN_POINT ( 'NONE',  ( 5.044974746830580337, 0.000000000000000000, -14.76997474683059153 ) ) ;
#13340=DIRECTION ( 'NONE',  ( -0.9740972002433518906, -0.2261297071993489949, -2.769290221138109488E-17 ) ) ;
#13364=ORIENTED_EDGE ( 'NONE', *, *, #7487, .T. ) ;
#13370=AXIS2_PLACEMENT_3D ( 'NONE', #11597, #11689, #2750 ) ;
#13408=AXIS2_PLACEMENT_3D ( 'NONE', #13666, #16151, #12538 ) ;
#13421=ORIENTED_EDGE ( 'NONE', *, *, #6474, .F. ) ;
#13429=ORIENTED_EDGE ( 'NONE', *, *, #1087, .F. ) ;
#13458=DIRECTION ( 'NONE',  ( 0.000000000000000000, 1.000000000000000000, 0.000000000000000000 ) ) ;
#13467=ORIENTED_EDGE ( 'NONE', *, *, #10247, .T. ) ;
#13491=ORIENTED_EDGE ( 'NONE', *, *, #15185, .F. ) ;
#13495=FACE_OUTER_BOUND ( 'NONE', #6270, .T. ) ;
#13527=VERTEX_POINT ( 'NONE', #4208 ) ;
#13580=CARTESIAN_POINT ( 'NONE',  ( 5.941205806953520074, 1.854262922671694143E-15, 15.14120580695351670 ) ) ;
#13584=ORIENTED_EDGE ( 'NONE', *, *, #7989, .T. ) ;
#13592=ORIENTED_EDGE ( 'NONE', *, *, #13162, .F. ) ;
#13603=DIRECTION ( 'NONE',  ( 1.000000000000000000, 0.000000000000000000, 0.000000000000000000 ) ) ;
#13612=EDGE_CURVE ( 'NONE', #9012, #5898, #4915, .T. ) ;
#13666=CARTESIAN_POINT ( 'NONE',  ( 1.224999999999999867, 0.000000000000000000, 0.000000000000000000 ) ) ;
#13700=ADVANCED_FACE ( 'NONE', ( #16057 ), #13714, .F. ) ;
#13707=DIRECTION ( 'NONE',  ( -1.000000000000000000, 0.000000000000000000, 0.000000000000000000 ) ) ;
#13711=ORIENTED_EDGE ( 'NONE', *, *, #15070, .F. ) ;
#13714=CONICAL_SURFACE ( 'NONE', #3290, 13.62500000000000000, 0.2281026282799422378 ) ;
#13721=EDGE_CURVE ( 'NONE', #16479, #6189, #4620, .T. ) ;
#13728=AXIS2_PLACEMENT_3D ( 'NONE', #7096, #5814, #11060 ) ;
#13735=CARTESIAN_POINT ( 'NONE',  ( -8.881784197001250351E-16, 0.000000000000000000, 0.000000000000000000 ) ) ;
#13745=DIRECTION ( 'NONE',  ( 0.000000000000000000, 1.000000000000000000, 0.000000000000000000 ) ) ;
#13750=DIRECTION ( 'NONE',  ( 0.000000000000000000, 1.000000000000000000, 0.000000000000000000 ) ) ;
#13762=DIRECTION ( 'NONE',  ( 0.000000000000000000, 1.000000000000000000, 0.000000000000000000 ) ) ;
#13763=ORIENTED_EDGE ( 'NONE', *, *, #15774, .F. ) ;
#13775=DIRECTION ( 'NONE',  ( 1.000000000000000000, 0.000000000000000000, 0.000000000000000000 ) ) ;
#13792=CONICAL_SURFACE ( 'NONE', #9129, 14.43750000000000000, 0.7483780475235185525 ) ;
#13805=EDGE_CURVE ( 'NONE', #2869, #6725, #8496, .T. ) ;
#13821=DIRECTION ( 'NONE',  ( 0.000000000000000000, 1.000000000000000000, 0.000000000000000000 ) ) ;
#13828=FACE_OUTER_BOUND ( 'NONE', #7850, .T. ) ;
#13840=ORIENTED_EDGE ( 'NONE', *, *, #6474, .T. ) ;
#13842=CARTESIAN_POINT ( 'NONE',  ( 5.945602903476760126, 0.000000000000000000, 0.000000000000000000 ) ) ;
#13921=DIRECTION ( 'NONE',  ( 0.000000000000000000, 1.000000000000000000, 0.000000000000000000 ) ) ;
#13942=CARTESIAN_POINT ( 'NONE',  ( 7.000000000000000000, -17.85000000000000142, -2.225795557450314789E-15 ) ) ;
#13958=ORIENTED_EDGE ( 'NONE', *, *, #7989, .F. ) ;
#13987=EDGE_LOOP ( 'NONE', ( #5158, #9452, #14690, #13467 ) ) ;
#14000=DIRECTION ( 'NONE',  ( -1.000000000000000000, 0.000000000000000000, 0.000000000000000000 ) ) ;
#14024=AXIS2_PLACEMENT_3D ( 'NONE', #8019, #46, #1159 ) ;
#14038=DIRECTION ( 'NONE',  ( 0.000000000000000000, 1.000000000000000000, 0.000000000000000000 ) ) ;
#14047=ORIENTED_EDGE ( 'NONE', *, *, #924, .F. ) ;
#14056=DIRECTION ( 'NONE',  ( 1.000000000000000000, 0.000000000000000000, 0.000000000000000000 ) ) ;
#14083=SURFACE_STYLE_USAGE ( .BOTH. , #15210 ) ;
#14106=AXIS2_PLACEMENT_3D ( 'NONE', #4725, #13603, #12384 ) ;
#14120=CARTESIAN_POINT ( 'NONE',  ( 1.574999999999999956, 0.000000000000000000, 0.000000000000000000 ) ) ;
#14149=ORIENTED_EDGE ( 'NONE', *, *, #8088, .F. ) ;
#14180=AXIS2_PLACEMENT_3D ( 'NONE', #8469, #13707, #1929 ) ;
#14187=ORIENTED_EDGE ( 'NONE', *, *, #1939, .T. ) ;
#14213=EDGE_CURVE ( 'NONE', #2814, #199, #16012, .T. ) ;
#14219=EDGE_CURVE ( 'NONE', #16915, #14244, #6810, .T. ) ;
#14244=VERTEX_POINT ( 'NONE', #8629 ) ;
#14283=DIRECTION ( 'NONE',  ( -1.000000000000000000, 0.000000000000000000, 0.000000000000000000 ) ) ;
#14318=VECTOR ( 'NONE', #11555, 1000.000000000000000 ) ;
#14319=VECTOR ( 'NONE', #10689, 1000.000000000000227 ) ;
#14330=CARTESIAN_POINT ( 'NONE',  ( 3.674999999999999822, 0.000000000000000000, 0.000000000000000000 ) ) ;
#14336=FACE_OUTER_BOUND ( 'NONE', #5232, .T. ) ;
#14338=CARTESIAN_POINT ( 'NONE',  ( 1.224999999999999867, 15.25000000000000000, 0.000000000000000000 ) ) ;
#14345=CIRCLE ( 'NONE', #3379, 0.5249999999999994671 ) ;
#14349=EDGE_LOOP ( 'NONE', ( #4059, #9245, #10429, #12311 ) ) ;
#14415=CARTESIAN_POINT ( 'NONE',  ( 1.750000000000000000, -14.59999999999999964, -1.827785347727424768E-15 ) ) ;
#14430=( NAMED_UNIT ( * ) SI_UNIT ( $, .STERADIAN. ) SOLID_ANGLE_UNIT ( ) );
#14483=ORIENTED_EDGE ( 'NONE', *, *, #1523, .T. ) ;
#14486=DIRECTION ( 'NONE',  ( 1.000000000000000000, 0.000000000000000000, 0.000000000000000000 ) ) ;
#14570=FACE_OUTER_BOUND ( 'NONE', #12292, .T. ) ;
#14586=CARTESIAN_POINT ( 'NONE',  ( 4.549999999999999822, 1.748183305782846567E-15, 14.27500000000000036 ) ) ;
#14588=DIRECTION ( 'NONE',  ( 0.000000000000000000, 1.000000000000000000, 0.000000000000000000 ) ) ;
#14590=VECTOR ( 'NONE', #16852, 1000.000000000000000 ) ;
#14609=ORIENTED_EDGE ( 'NONE', *, *, #11915, .T. ) ;
#14623=TOROIDAL_SURFACE ( 'NONE', #10789, 14.76997474683060041, 0.5250000000000000222 ) ;
#14628=VERTEX_POINT ( 'NONE', #4795 ) ;
#14630=CIRCLE ( 'NONE', #12989, 12.00000000000000000 ) ;
#14684=CARTESIAN_POINT ( 'NONE',  ( 1.050000000000000044, 0.000000000000000000, 0.000000000000000000 ) ) ;
#14690=ORIENTED_EDGE ( 'NONE', *, *, #14219, .T. ) ;
#14693=TOROIDAL_SURFACE ( 'NONE', #7265, 14.76997474683060041, 0.5250000000000000222 ) ;
#14725=ORIENTED_EDGE ( 'NONE', *, *, #7204, .T. ) ;
#14759=FACE_OUTER_BOUND ( 'NONE', #4731, .T. ) ;
#14772=ORIENTED_EDGE ( 'NONE', *, *, #16690, .T. ) ;
#14778=DIRECTION ( 'NONE',  ( 1.000000000000000000, 0.000000000000000000, 0.000000000000000000 ) ) ;
#14791=CIRCLE ( 'NONE', #2985, 14.27500000000000036 ) ;
#14794=EDGE_LOOP ( 'NONE', ( #10536, #11664, #8360, #6442 ) ) ;
#14822=LINE ( 'NONE', #6814, #2975 ) ;
#14828=LINE ( 'NONE', #2712, #9124 ) ;
#14837=EDGE_CURVE ( 'NONE', #6189, #13527, #4951, .T. ) ;
#14854=DIRECTION ( 'NONE',  ( 1.000000000000000000, 0.000000000000000000, 0.000000000000000000 ) ) ;
#14877=ORIENTED_EDGE ( 'NONE', *, *, #14837, .F. ) ;
#14881=ADVANCED_FACE ( 'NONE', ( #14759 ), #2982, .T. ) ;
#14890=FILL_AREA_STYLE ('',( #6000 ) ) ;
#14907=DIRECTION ( 'NONE',  ( 0.000000000000000000, 1.000000000000000000, 0.000000000000000000 ) ) ;
#14912=CONICAL_SURFACE ( 'NONE', #8032, 12.97499999999999964, 0.5543074962015517304 ) ;
#14919=AXIS2_PLACEMENT_3D ( 'NONE', #7485, #5001, #8886 ) ;
#14924=CARTESIAN_POINT ( 'NONE',  ( 5.044974746830580337, 0.000000000000000000, 0.000000000000000000 ) ) ;
#15004=ORIENTED_EDGE ( 'NONE', *, *, #15086, .T. ) ;
#15008=VECTOR ( 'NONE', #5634, 1000.000000000000000 ) ;
#15043=CARTESIAN_POINT ( 'NONE',  ( 7.000000000000000000, 17.52499999999999858, 0.000000000000000000 ) ) ;
#15067=EDGE_CURVE ( 'NONE', #13527, #11643, #3114, .T. ) ;
#15070=EDGE_CURVE ( 'NONE', #5898, #9012, #5018, .T. ) ;
#15086=EDGE_CURVE ( 'NONE', #155, #12375, #14345, .T. ) ;
#15088=CYLINDRICAL_SURFACE ( 'NONE', #12266, 18.50000000000000000 ) ;
#15096=CARTESIAN_POINT ( 'NONE',  ( 0.3499999999999999778, -18.17500000000000071, 2.225795557450314789E-15 ) ) ;
#15097=EDGE_LOOP ( 'NONE', ( #1587, #5679, #7032, #14877 ) ) ;
#15119=CIRCLE ( 'NONE', #16225, 18.50000000000000000 ) ;
#15124=AXIS2_PLACEMENT_3D ( 'NONE', #5212, #1704, #1539 ) ;
#15164=ORIENTED_EDGE ( 'NONE', *, *, #15067, .F. ) ;
#15185=EDGE_CURVE ( 'NONE', #16479, #6787, #2529, .T. ) ;
#15210=SURFACE_SIDE_STYLE ('',( #11246 ) ) ;
#15212=VERTEX_POINT ( 'NONE', #6550 ) ;
#15217=DIRECTION ( 'NONE',  ( 1.000000000000000000, 0.000000000000000000, 0.000000000000000000 ) ) ;
#15218=CONICAL_SURFACE ( 'NONE', #15756, 13.89560290347679938, 1.567266246505109928 ) ;
#15238=DIRECTION ( 'NONE',  ( 0.000000000000000000, 1.000000000000000000, 0.000000000000000000 ) ) ;
#15276=DIRECTION ( 'NONE',  ( -0.7327934916262990317, -0.6804510993672779895, -8.333122608164345406E-17 ) ) ;
#15339=DIRECTION ( 'NONE',  ( 1.000000000000000000, 0.000000000000000000, 0.000000000000000000 ) ) ;
#15357=EDGE_CURVE ( 'NONE', #16649, #11007, #3391, .T. ) ;
#15360=AXIS2_PLACEMENT_3D ( 'NONE', #8311, #6674, #424 ) ;
#15370=DIRECTION ( 'NONE',  ( 1.000000000000000000, 0.000000000000000000, 0.000000000000000000 ) ) ;
#15444=AXIS2_PLACEMENT_3D ( 'NONE', #3991, #2427, #1146 ) ;
#15494=FACE_OUTER_BOUND ( 'NONE', #16009, .T. ) ;
#15505=EDGE_CURVE ( 'NONE', #11290, #11248, #4590, .T. ) ;
#15512=ORIENTED_EDGE ( 'NONE', *, *, #7068, .F. ) ;
#15517=ORIENTED_EDGE ( 'NONE', *, *, #5725, .T. ) ;
#15542=CIRCLE ( 'NONE', #11152, 18.50000000000000000 ) ;
#15576=DIRECTION ( 'NONE',  ( 0.000000000000000000, 1.000000000000000000, 0.000000000000000000 ) ) ;
#15594=DIRECTION ( 'NONE',  ( 1.000000000000000000, 0.000000000000000000, 0.000000000000000000 ) ) ;
#15614=DIRECTION ( 'NONE',  ( 0.000000000000000000, 1.000000000000000000, 0.000000000000000000 ) ) ;
#15621=( NAMED_UNIT ( * ) SI_UNIT ( $, .STERADIAN. ) SOLID_ANGLE_UNIT ( ) );
#15636=CIRCLE ( 'NONE', #15360, 15.14120580695350071 ) ;
#15658=ADVANCED_FACE ( 'NONE', ( #11615 ), #4499, .T. ) ;
#15708=EDGE_CURVE ( 'NONE', #15212, #7469, #16082, .T. ) ;
#15740=FACE_OUTER_BOUND ( 'NONE', #3655, .T. ) ;
#15756=AXIS2_PLACEMENT_3D ( 'NONE', #13842, #6004, #13750 ) ;
#15774=EDGE_CURVE ( 'NONE', #5894, #2869, #16032, .T. ) ;
#15788=( NAMED_UNIT ( * ) PLANE_ANGLE_UNIT ( ) SI_UNIT ( $, .RADIAN. ) );
#15790=EDGE_LOOP ( 'NONE', ( #4410, #11140, #14725, #3878 ) ) ;
#15791=VECTOR ( 'NONE', #13132, 1000.000000000000114 ) ;
#15808=DIRECTION ( 'NONE',  ( 0.000000000000000000, 1.000000000000000000, 0.000000000000000000 ) ) ;
#15810=CARTESIAN_POINT ( 'NONE',  ( 2.625000000000000000, -14.59999999999999964, -1.787984326755135766E-15 ) ) ;
#15812=EDGE_LOOP ( 'NONE', ( #13042, #10962, #1551, #6351 ) ) ;
#15834=LINE ( 'NONE', #9486, #9408 ) ;
#15882=DIRECTION ( 'NONE',  ( -1.000000000000000000, 2.277380563333649802E-16, 0.000000000000000000 ) ) ;
#15895=EDGE_CURVE ( 'NONE', #117, #10651, #4511, .T. ) ;
#15921=VERTEX_POINT ( 'NONE', #11014 ) ;
#15957=TOROIDAL_SURFACE ( 'NONE', #9379, 14.27500000000000036, 0.6999999999999999556 ) ;
#16009=EDGE_LOOP ( 'NONE', ( #16751, #6075, #9255, #10238 ) ) ;
#16012=LINE ( 'NONE', #2875, #2807 ) ;
#16019=DIRECTION ( 'NONE',  ( 0.000000000000000000, 1.000000000000000000, 0.000000000000000000 ) ) ;
#16032=CIRCLE ( 'NONE', #1770, 14.27500000000000036 ) ;
#16038=VECTOR ( 'NONE', #7429, 1000.000000000000000 ) ;
#16045=ORIENTED_EDGE ( 'NONE', *, *, #2005, .T. ) ;
#16053=LINE ( 'NONE', #15096, #1309 ) ;
#16057=FACE_OUTER_BOUND ( 'NONE', #5527, .T. ) ;
#16078=CIRCLE ( 'NONE', #10875, 12.64814671169700055 ) ;
#16082=LINE ( 'NONE', #6793, #2034 ) ;
#16091=ORIENTED_EDGE ( 'NONE', *, *, #13721, .F. ) ;
#16143=EDGE_CURVE ( 'NONE', #14628, #6725, #12743, .T. ) ;
#16151=DIRECTION ( 'NONE',  ( -1.000000000000000000, 0.000000000000000000, 0.000000000000000000 ) ) ;
#16157=DIRECTION ( 'NONE',  ( 1.000000000000000000, 0.000000000000000000, 0.000000000000000000 ) ) ;
#16161=VERTEX_POINT ( 'NONE', #13066 ) ;
#16175=ORIENTED_EDGE ( 'NONE', *, *, #7758, .T. ) ;
#16187=CARTESIAN_POINT ( 'NONE',  ( 5.941205806953520074, 15.14120580695428764, 0.000000000000000000 ) ) ;
#16225=AXIS2_PLACEMENT_3D ( 'NONE', #6112, #1921, #15238 ) ;
#16240=ORIENTED_EDGE ( 'NONE', *, *, #9737, .F. ) ;
#16261=ORIENTED_EDGE ( 'NONE', *, *, #4132, .F. ) ;
#16302=CYLINDRICAL_SURFACE ( 'NONE', #13728, 17.52499999999999858 ) ;
#16305=DIRECTION ( 'NONE',  ( 0.000000000000000000, 1.000000000000000000, 0.000000000000000000 ) ) ;
#16312=DIRECTION ( 'NONE',  ( 0.6294249519366466039, 0.7770612780724246438, 0.000000000000000000 ) ) ;
#16342=CARTESIAN_POINT ( 'NONE',  ( 5.569974746830579804, 1.808800229719333629E-15, 14.76997474683060041 ) ) ;
#16389=EDGE_LOOP ( 'NONE', ( #5952, #4939 ) ) ;
#16395=ORIENTED_EDGE ( 'NONE', *, *, #8529, .T. ) ;
#16441=ORIENTED_EDGE ( 'NONE', *, *, #3543, .T. ) ;
#16447=CARTESIAN_POINT ( 'NONE',  ( -1.776356839400249676E-15, -13.94999999999999929, -1.708382284810557762E-15 ) ) ;
#16454=CARTESIAN_POINT ( 'NONE',  ( -1.776356839400249676E-15, 0.000000000000000000, 0.000000000000000000 ) ) ;
#16460=DIRECTION ( 'NONE',  ( -1.000000000000000000, 0.000000000000000000, 0.000000000000000000 ) ) ;
#16469=CARTESIAN_POINT ( 'NONE',  ( 5.162501635565829972, 12.32407335584850117, 0.000000000000000000 ) ) ;
#16479=VERTEX_POINT ( 'NONE', #2533 ) ;
#16495=DIRECTION ( 'NONE',  ( 0.000000000000000000, 1.000000000000000000, -1.224646799147353207E-16 ) ) ;
#16530=FACE_OUTER_BOUND ( 'NONE', #6867, .T. ) ;
#16534=AXIS2_PLACEMENT_3D ( 'NONE', #8450, #14000, #6247 ) ;
#16540=EDGE_CURVE ( 'NONE', #11116, #16479, #14630, .T. ) ;
#16564=DIRECTION ( 'NONE',  ( 0.000000000000000000, 0.000000000000000000, -1.000000000000000000 ) ) ;
#16649=VERTEX_POINT ( 'NONE', #16187 ) ;
#16658=ADVANCED_FACE ( 'NONE', ( #1677 ), #10874, .F. ) ;
#16687=DIRECTION ( 'NONE',  ( 0.000000000000000000, 1.000000000000000000, 0.000000000000000000 ) ) ;
#16690=EDGE_CURVE ( 'NONE', #10651, #117, #4746, .T. ) ;
#16737=EDGE_CURVE ( 'NONE', #2600, #7389, #2556, .T. ) ;
#16751=ORIENTED_EDGE ( 'NONE', *, *, #10062, .F. ) ;
#16774=AXIS2_PLACEMENT_3D ( 'NONE', #4092, #1427, #5635 ) ;
#16794=FACE_OUTER_BOUND ( 'NONE', #5252, .T. ) ;
#16836=CARTESIAN_POINT ( 'NONE',  ( 2.625000000000000000, 0.000000000000000000, 0.000000000000000000 ) ) ;
#16852=DIRECTION ( 'NONE',  ( -1.000000000000000000, 0.000000000000000000, 0.000000000000000000 ) ) ;
#16869=ORIENTED_EDGE ( 'NONE', *, *, #9737, .T. ) ;
#16895=CARTESIAN_POINT ( 'NONE',  ( 1.399999999999999911, 13.62500000000000000, 0.000000000000000000 ) ) ;
#16913=CARTESIAN_POINT ( 'NONE',  ( 5.162501635565829972, 0.000000000000000000, 0.000000000000000000 ) ) ;
#16915=VERTEX_POINT ( 'NONE', #2257 ) ;
#16927=EDGE_CURVE ( 'NONE', #2869, #12856, #12719, .T. ) ;
ENDSEC;
END-ISO-10303-21;
